ISO-10303-21;
HEADER;
FILE_DESCRIPTION (('STEP AP214'),
    '1' );
FILE_NAME ('Body.step',
    '2026-10-22T18:53:08',
    ( '' ),
    ( '' ),
    'SwSTEP 2.0',
    'SolidWorks 2025',
    '' );
FILE_SCHEMA (( 'AUTOMOTIVE_DESIGN' ));
ENDSEC;

DATA;
#2=DIRECTION ( 'NONE',  ( -0.000000000000000000, -0.000000000000000000, -1.000000000000000000 ) ) ;
#14=VERTEX_POINT ( 'NONE', #7795 ) ;
#23=LINE ( 'NONE', #14874, #8703 ) ;
#28=VECTOR ( 'NONE', #2460, 1000.000000000000000 ) ;
#30=ORIENTED_EDGE ( 'NONE', *, *, #13409, .T. ) ;
#49=EDGE_LOOP ( 'NONE', ( #12692, #15441, #20790, #14111 ) ) ;
#55=ORIENTED_EDGE ( 'NONE', *, *, #9968, .T. ) ;
#57=CIRCLE ( 'NONE', #17578, 23.85000000000000497 ) ;
#63=EDGE_CURVE ( 'NONE', #8004, #14530, #22184, .T. ) ;
#68=ORIENTED_EDGE ( 'NONE', *, *, #149, .T. ) ;
#79=LINE ( 'NONE', #7484, #19699 ) ;
#87=DIRECTION ( 'NONE',  ( 1.000000000000000000, 0.000000000000000000, 0.000000000000000000 ) ) ;
#103=AXIS2_PLACEMENT_3D ( 'NONE', #19821, #17978, #17736 ) ;
#106=ORIENTED_EDGE ( 'NONE', *, *, #4031, .T. ) ;
#107=VECTOR ( 'NONE', #16145, 1000.000000000000000 ) ;
#113=CARTESIAN_POINT ( 'NONE',  ( -23.84999999999999432, -15.03999999999999915, 27.00000000000000000 ) ) ;
#116=LINE ( 'NONE', #7524, #12182 ) ;
#124=CARTESIAN_POINT ( 'NONE',  ( -17.32314925601269451, 8.733074366907754182, 3.769949228126193930 ) ) ;
#128=VERTEX_POINT ( 'NONE', #9516 ) ;
#129=CARTESIAN_POINT ( 'NONE',  ( -14.99999999999999822, 0.000000000000000000, 27.00000000000000000 ) ) ;
#149=EDGE_CURVE ( 'NONE', #1960, #22892, #17041, .T. ) ;
#151=DIRECTION ( 'NONE',  ( -0.000000000000000000, -0.000000000000000000, 1.000000000000000000 ) ) ;
#178=CIRCLE ( 'NONE', #11833, 18.49999999999999645 ) ;
#184=DIRECTION ( 'NONE',  ( -0.000000000000000000, -0.000000000000000000, -1.000000000000000000 ) ) ;
#186=EDGE_CURVE ( 'NONE', #13664, #23091, #13200, .T. ) ;
#201=PRODUCT_CONTEXT ( 'NONE', #6527, 'mechanical' ) ;
#222=CARTESIAN_POINT ( 'NONE',  ( 0.000000000000000000, -45.00000000000000000, 23.99999999999999645 ) ) ;
#230=VERTEX_POINT ( 'NONE', #4246 ) ;
#233=CARTESIAN_POINT ( 'NONE',  ( 39.99999999999999289, 29.50000000000000000, 27.00000000000000000 ) ) ;
#251=EDGE_CURVE ( 'NONE', #498, #18820, #12021, .T. ) ;
#252=CARTESIAN_POINT ( 'NONE',  ( -17.15242344757784565, 8.297343789534778580, -4.632629386303500851 ) ) ;
#259=ORIENTED_EDGE ( 'NONE', *, *, #11803, .F. ) ;
#265=DIRECTION ( 'NONE',  ( 1.000000000000000000, 0.000000000000000000, 0.000000000000000000 ) ) ;
#279=FACE_BOUND ( 'NONE', #20917, .T. ) ;
#297=DIRECTION ( 'NONE',  ( -0.7071067811865469066, 8.659560562354941486E-17, -0.7071067811865482389 ) ) ;
#301=EDGE_LOOP ( 'NONE', ( #1823, #10414, #21595, #8457 ) ) ;
#303=ORIENTED_EDGE ( 'NONE', *, *, #17244, .F. ) ;
#308=ORIENTED_EDGE ( 'NONE', *, *, #9116, .T. ) ;
#327=CIRCLE ( 'NONE', #7697, 5.100000000000000533 ) ;
#328=CARTESIAN_POINT ( 'NONE',  ( 20.84999999999999432, -15.04000000000000270, -25.00000000000000000 ) ) ;
#346=EDGE_CURVE ( 'NONE', #5306, #13831, #14026, .T. ) ;
#347=CARTESIAN_POINT ( 'NONE',  ( 29.00000000000000355, 29.50000000000000000, 27.00000000000000000 ) ) ;
#348=CARTESIAN_POINT ( 'NONE',  ( 0.000000000000000000, 15.03999999999999915, 25.00000000000000000 ) ) ;
#350=CARTESIAN_POINT ( 'NONE',  ( 41.50000000000000000, -27.79189783386526358, 27.00000000000000000 ) ) ;
#352=CARTESIAN_POINT ( 'NONE',  ( -23.85000000000000497, 15.03999999999999915, 25.00000000000000000 ) ) ;
#353=EDGE_LOOP ( 'NONE', ( #15923, #14823, #11510, #16658 ) ) ;
#354=DIRECTION ( 'NONE',  ( 0.000000000000000000, 0.000000000000000000, 1.000000000000000000 ) ) ;
#355=LINE ( 'NONE', #16801, #10958 ) ;
#357=CARTESIAN_POINT ( 'NONE',  ( -16.44572538483723534, 6.755397553796130161, -6.683320200552557822 ) ) ;
#372=DIRECTION ( 'NONE',  ( -0.000000000000000000, -0.000000000000000000, -1.000000000000000000 ) ) ;
#376=CARTESIAN_POINT ( 'NONE',  ( 14.98952570844870102, -0.6468970097546504761, -9.483487670324114660 ) ) ;
#382=CARTESIAN_POINT ( 'NONE',  ( -31.10231664966676135, -45.36128193761570770, -27.00000000000000000 ) ) ;
#389=LINE ( 'NONE', #19303, #6735 ) ;
#392=DIRECTION ( 'NONE',  ( -1.000000000000000000, 0.000000000000000000, 0.000000000000000000 ) ) ;
#409=DIRECTION ( 'NONE',  ( -1.000000000000000000, -0.000000000000000000, -0.000000000000000000 ) ) ;
#410=DIRECTION ( 'NONE',  ( -0.000000000000000000, -0.000000000000000000, -1.000000000000000000 ) ) ;
#414=DIRECTION ( 'NONE',  ( -1.000000000000000000, -0.000000000000000000, -0.000000000000000000 ) ) ;
#415=DIRECTION ( 'NONE',  ( -1.000000000000000000, 0.000000000000000000, 0.000000000000000000 ) ) ;
#416=DIRECTION ( 'NONE',  ( 1.000000000000000000, 0.000000000000000000, 0.000000000000000000 ) ) ;
#442=CARTESIAN_POINT ( 'NONE',  ( 0.000000000000000000, 45.00000000000000000, -23.99999999999999645 ) ) ;
#449=CARTESIAN_POINT ( 'NONE',  ( -41.99999999999999289, 0.000000000000000000, 10.50249999999999950 ) ) ;
#455=CONICAL_SURFACE ( 'NONE', #13345, 10.50249999999999950, 0.7853981633974491672 ) ;
#459=CARTESIAN_POINT ( 'NONE',  ( -39.99999999999999289, 27.79189783386526358, -27.00000000000000000 ) ) ;
#476=EDGE_CURVE ( 'NONE', #5201, #9670, #7337, .T. ) ;
#484=EDGE_LOOP ( 'NONE', ( #7271, #13067, #20079, #19929 ) ) ;
#490=DIRECTION ( 'NONE',  ( 0.000000000000000000, 0.000000000000000000, 1.000000000000000000 ) ) ;
#498=VERTEX_POINT ( 'NONE', #8959 ) ;
#516=CARTESIAN_POINT ( 'NONE',  ( -40.89823313241237912, -26.41789760203349502, 27.00000000000000000 ) ) ;
#526=CIRCLE ( 'NONE', #18452, 18.49999999999999645 ) ;
#529=ORIENTED_EDGE ( 'NONE', *, *, #1014, .F. ) ;
#544=DIRECTION ( 'NONE',  ( -0.000000000000000000, -0.000000000000000000, 1.000000000000000000 ) ) ;
#569=VERTEX_POINT ( 'NONE', #6215 ) ;
#570=CARTESIAN_POINT ( 'NONE',  ( -1.029124893018731811E-15, -45.00000000000000000, -22.79827876194487857 ) ) ;
#585=AXIS2_PLACEMENT_3D ( 'NONE', #2571, #21363, #17444 ) ;
#588=VERTEX_POINT ( 'NONE', #4531 ) ;
#615=AXIS2_PLACEMENT_3D ( 'NONE', #6424, #7742, #9691 ) ;
#616=ORIENTED_EDGE ( 'NONE', *, *, #19811, .F. ) ;
#617=AXIS2_PLACEMENT_3D ( 'NONE', #4422, #21255, #2953 ) ;
#624=DIRECTION ( 'NONE',  ( -0.7071067811865660024, 8.659560562355159656E-17, 0.7071067811865291430 ) ) ;
#632=FACE_OUTER_BOUND ( 'NONE', #10818, .T. ) ;
#634=ORIENTED_EDGE ( 'NONE', *, *, #9707, .T. ) ;
#636=CARTESIAN_POINT ( 'NONE',  ( 0.000000000000000000, 15.23000000000000220, -27.00000000000000000 ) ) ;
#646=DIRECTION ( 'NONE',  ( -1.000000000000000000, 0.000000000000000000, -0.000000000000000000 ) ) ;
#678=VERTEX_POINT ( 'NONE', #13306 ) ;
#682=ORIENTED_EDGE ( 'NONE', *, *, #20570, .T. ) ;
#683=ORIENTED_EDGE ( 'NONE', *, *, #3175, .F. ) ;
#688=EDGE_CURVE ( 'NONE', #12983, #14507, #3818, .T. ) ;
#691=CARTESIAN_POINT ( 'NONE',  ( 20.85000000000000853, 15.03999999999999915, 25.00000000000000000 ) ) ;
#699=CARTESIAN_POINT ( 'NONE',  ( -28.27483331787887266, 41.23752903419610760, 27.00000000000000000 ) ) ;
#700=DIRECTION ( 'NONE',  ( 0.000000000000000000, 0.000000000000000000, -1.000000000000000000 ) ) ;
#704=VERTEX_POINT ( 'NONE', #13192 ) ;
#709=ORIENTED_EDGE ( 'NONE', *, *, #20639, .T. ) ;
#713=CARTESIAN_POINT ( 'NONE',  ( -41.99999999999999289, -25.93535998569255341, 27.00000000000000000 ) ) ;
#715=ADVANCED_FACE ( 'NONE', ( #22496 ), #5772, .F. ) ;
#720=ORIENTED_EDGE ( 'NONE', *, *, #688, .F. ) ;
#721=VERTEX_POINT ( 'NONE', #7935 ) ;
#726=DIRECTION ( 'NONE',  ( -1.337728473353585242E-16, 1.000000000000000000, -0.000000000000000000 ) ) ;
#727=FACE_OUTER_BOUND ( 'NONE', #2742, .T. ) ;
#731=AXIS2_PLACEMENT_3D ( 'NONE', #7093, #20394, #22131 ) ;
#732=VERTEX_POINT ( 'NONE', #13445 ) ;
#746=ORIENTED_EDGE ( 'NONE', *, *, #10848, .F. ) ;
#755=EDGE_CURVE ( 'NONE', #22742, #3887, #21498, .T. ) ;
#756=DIRECTION ( 'NONE',  ( 0.000000000000000000, 1.000000000000000000, 0.000000000000000000 ) ) ;
#760=VERTEX_POINT ( 'NONE', #13943 ) ;
#765=DIRECTION ( 'NONE',  ( -1.000000000000000000, -0.000000000000000000, -0.000000000000000000 ) ) ;
#785=ORIENTED_EDGE ( 'NONE', *, *, #16933, .F. ) ;
#803=CARTESIAN_POINT ( 'NONE',  ( -16.18147534945000032, -6.260849737139247750, 7.148624562014530781 ) ) ;
#826=ORIENTED_EDGE ( 'NONE', *, *, #3707, .T. ) ;
#841=ORIENTED_EDGE ( 'NONE', *, *, #22771, .T. ) ;
#850=DIRECTION ( 'NONE',  ( -0.000000000000000000, -0.000000000000000000, -1.000000000000000000 ) ) ;
#854=DIRECTION ( 'NONE',  ( 0.9160001545545232160, 0.4011779117250717785, 0.000000000000000000 ) ) ;
#886=VERTEX_POINT ( 'NONE', #10737 ) ;
#905=ADVANCED_FACE ( 'NONE', ( #1846 ), #14401, .F. ) ;
#913=EDGE_LOOP ( 'NONE', ( #1338, #8471, #1416 ) ) ;
#915=AXIS2_PLACEMENT_3D ( 'NONE', #442, #15301, #22902 ) ;
#918=ORIENTED_EDGE ( 'NONE', *, *, #23641, .F. ) ;
#925=DIRECTION ( 'NONE',  ( 0.000000000000000000, 0.000000000000000000, 1.000000000000000000 ) ) ;
#928=CARTESIAN_POINT ( 'NONE',  ( -15.78970982176773319, -5.581464347350857835, -7.700125654604357273 ) ) ;
#941=DIRECTION ( 'NONE',  ( -0.000000000000000000, -0.000000000000000000, -1.000000000000000000 ) ) ;
#947=EDGE_LOOP ( 'NONE', ( #13196, #14104, #14559, #19389 ) ) ;
#953=ORIENTED_EDGE ( 'NONE', *, *, #12676, .F. ) ;
#954=FACE_BOUND ( 'NONE', #5585, .T. ) ;
#959=FACE_OUTER_BOUND ( 'NONE', #22292, .T. ) ;
#966=CARTESIAN_POINT ( 'NONE',  ( 0.000000000000000000, -45.00000000000000000, 27.00000000000000000 ) ) ;
#969=ORIENTED_EDGE ( 'NONE', *, *, #16996, .T. ) ;
#973=CARTESIAN_POINT ( 'NONE',  ( -23.85000000000000497, 15.03999999999999915, -27.00000000000000000 ) ) ;
#982=ORIENTED_EDGE ( 'NONE', *, *, #12348, .T. ) ;
#992=EDGE_CURVE ( 'NONE', #20705, #4244, #3436, .T. ) ;
#994=ORIENTED_EDGE ( 'NONE', *, *, #19149, .F. ) ;
#996=CARTESIAN_POINT ( 'NONE',  ( 0.000000000000000000, 0.000000000000000000, 27.00000000000000000 ) ) ;
#998=VECTOR ( 'NONE', #5419, 1000.000000000000000 ) ;
#999=DIRECTION ( 'NONE',  ( -1.000000000000000000, 0.000000000000000000, 0.000000000000000000 ) ) ;
#1001=CIRCLE ( 'NONE', #11092, 10.50249999999999950 ) ;
#1002=LINE ( 'NONE', #2950, #14791 ) ;
#1014=EDGE_CURVE ( 'NONE', #4702, #7988, #1279, .T. ) ;
#1030=DIRECTION ( 'NONE',  ( -0.9160001545545232160, -0.4011779117250717785, 0.000000000000000000 ) ) ;
#1046=AXIS2_PLACEMENT_3D ( 'NONE', #5008, #14371, #21828 ) ;
#1060=DIRECTION ( 'NONE',  ( 4.613626265895763066E-16, 1.000000000000000000, 0.000000000000000000 ) ) ;
#1066=CARTESIAN_POINT ( 'NONE',  ( -30.44534269664590198, -40.40463133211081015, 27.00000000000000000 ) ) ;
#1097=CARTESIAN_POINT ( 'NONE',  ( 0.000000000000000000, 0.000000000000000000, 27.00000000000000000 ) ) ;
#1107=AXIS2_PLACEMENT_3D ( 'NONE', #18511, #13000, #18268 ) ;
#1110=DIRECTION ( 'NONE',  ( -0.000000000000000000, -0.000000000000000000, 1.000000000000000000 ) ) ;
#1118=DIRECTION ( 'NONE',  ( -1.000000000000000000, 0.000000000000000000, 0.000000000000000000 ) ) ;
#1128=ORIENTED_EDGE ( 'NONE', *, *, #11602, .F. ) ;
#1135=DIRECTION ( 'NONE',  ( 1.000000000000000000, 0.000000000000000000, 0.000000000000000000 ) ) ;
#1147=ORIENTED_EDGE ( 'NONE', *, *, #10934, .T. ) ;
#1161=LINE ( 'NONE', #10416, #16200 ) ;
#1172=DIRECTION ( 'NONE',  ( -0.000000000000000000, -0.000000000000000000, -1.000000000000000000 ) ) ;
#1174=CARTESIAN_POINT ( 'NONE',  ( -17.05196227081077609, -8.053793831531462999, 5.044162359773902260 ) ) ;
#1183=CARTESIAN_POINT ( 'NONE',  ( 16.36153765883234712, -6.593687918952693572, -6.842832175870683820 ) ) ;
#1193=DIRECTION ( 'NONE',  ( 0.000000000000000000, 0.000000000000000000, 1.000000000000000000 ) ) ;
#1195=ORIENTED_EDGE ( 'NONE', *, *, #63, .T. ) ;
#1198=CIRCLE ( 'NONE', #3135, 20.85000000000000142 ) ;
#1212=ADVANCED_FACE ( 'NONE', ( #14618 ), #14375, .F. ) ;
#1213=FACE_OUTER_BOUND ( 'NONE', #5508, .T. ) ;
#1227=CARTESIAN_POINT ( 'NONE',  ( 28.27483331787887622, 41.23752903419610050, 27.00000000000000000 ) ) ;
#1241=DIRECTION ( 'NONE',  ( -0.000000000000000000, -0.000000000000000000, -1.000000000000000000 ) ) ;
#1272=DIRECTION ( 'NONE',  ( -0.000000000000000000, -0.000000000000000000, -1.000000000000000000 ) ) ;
#1279=CIRCLE ( 'NONE', #6316, 9.499999999999994671 ) ;
#1290=CARTESIAN_POINT ( 'NONE',  ( 20.84999999999999432, -15.04000000000000448, -25.00000000000000000 ) ) ;
#1296=CARTESIAN_POINT ( 'NONE',  ( -14.51962751333973856, 3.765689428759025681, 8.721787840009204373 ) ) ;
#1297=CYLINDRICAL_SURFACE ( 'NONE', #8148, 14.99999999999999822 ) ;
#1299=CARTESIAN_POINT ( 'NONE',  ( -14.79227890392045275, -2.568991289487079221, 9.169086800441911933 ) ) ;
#1300=B_SPLINE_CURVE_WITH_KNOTS ( 'NONE', 3,
 ( #11944, #19410, #376, #13420, #21362, #2686, #15731, #4653 ),
 .UNSPECIFIED., .F., .F.,
 ( 4, 2, 2, 4 ),
 ( 0.003892319173193277415, 0.004864202078960305070, 0.005836084984727332725, 0.007779850796261388902 ),
 .UNSPECIFIED. ) ;
#1304=CIRCLE ( 'NONE', #18051, 2.024999999999999911 ) ;
#1309=VECTOR ( 'NONE', #20266, 1000.000000000000000 ) ;
#1318=CARTESIAN_POINT ( 'NONE',  ( -41.99999999999999289, 25.93535998569253920, 27.00000000000000000 ) ) ;
#1322=VECTOR ( 'NONE', #1861, 1000.000000000000000 ) ;
#1336=CARTESIAN_POINT ( 'NONE',  ( 17.52854577772373190, 9.313395544511452684, 1.935253206038901608 ) ) ;
#1338=ORIENTED_EDGE ( 'NONE', *, *, #16996, .F. ) ;
#1342=ORIENTED_EDGE ( 'NONE', *, *, #15135, .T. ) ;
#1343=ORIENTED_EDGE ( 'NONE', *, *, #22854, .F. ) ;
#1371=CARTESIAN_POINT ( 'NONE',  ( -14.51962751333973856, 3.765689428759025681, 8.721787840009204373 ) ) ;
#1387=DIRECTION ( 'NONE',  ( -0.7071067811865660024, 8.659560562355159656E-17, 0.7071067811865291430 ) ) ;
#1393=CYLINDRICAL_SURFACE ( 'NONE', #2791, 18.50000000000000000 ) ;
#1397=CIRCLE ( 'NONE', #15795, 2.024999999999999911 ) ;
#1402=EDGE_LOOP ( 'NONE', ( #19618, #10972, #14817, #21504 ) ) ;
#1410=ADVANCED_FACE ( 'NONE', ( #22640 ), #5922, .F. ) ;
#1411=EDGE_CURVE ( 'NONE', #11194, #10631, #9687, .T. ) ;
#1414=AXIS2_PLACEMENT_3D ( 'NONE', #10150, #13966, #15912 ) ;
#1416=ORIENTED_EDGE ( 'NONE', *, *, #2608, .T. ) ;
#1433=CARTESIAN_POINT ( 'NONE',  ( 14.51962751333974211, -3.765689428759034563, 8.721787840009190163 ) ) ;
#1434=VECTOR ( 'NONE', #8639, 1000.000000000000000 ) ;
#1442=ADVANCED_FACE ( 'NONE', ( #13204 ), #455, .F. ) ;
#1446=DIRECTION ( 'NONE',  ( 1.000000000000000000, 0.000000000000000000, 0.000000000000000000 ) ) ;
#1448=EDGE_LOOP ( 'NONE', ( #8557, #14312, #18773, #7041 ) ) ;
#1449=DIRECTION ( 'NONE',  ( -0.000000000000000000, -0.000000000000000000, -1.000000000000000000 ) ) ;
#1455=LINE ( 'NONE', #8863, #2548 ) ;
#1457=ORIENTED_EDGE ( 'NONE', *, *, #8924, .F. ) ;
#1461=DIRECTION ( 'NONE',  ( 1.000000000000000000, 0.000000000000000000, 0.000000000000000000 ) ) ;
#1463=CARTESIAN_POINT ( 'NONE',  ( 17.05196227081078320, 8.053793831531466552, 5.044162359773899595 ) ) ;
#1474=ORIENTED_EDGE ( 'NONE', *, *, #8163, .T. ) ;
#1475=ADVANCED_FACE ( 'NONE', ( #20279 ), #1393, .F. ) ;
#1493=DIRECTION ( 'NONE',  ( 1.000000000000000000, 0.000000000000000000, 0.000000000000000000 ) ) ;
#1515=CARTESIAN_POINT ( 'NONE',  ( 30.44534269664590909, -40.40463133211080304, 27.00000000000000000 ) ) ;
#1518=CARTESIAN_POINT ( 'NONE',  ( 41.99999999999999289, 5.618459588085056979E-15, -10.50249999999999950 ) ) ;
#1525=DIRECTION ( 'NONE',  ( -0.000000000000000000, -0.000000000000000000, 1.000000000000000000 ) ) ;
#1527=ORIENTED_EDGE ( 'NONE', *, *, #4652, .T. ) ;
#1529=CARTESIAN_POINT ( 'NONE',  ( -15.07341617659254318, -4.495283618570418582, -8.379779594489216166 ) ) ;
#1556=DIRECTION ( 'NONE',  ( -1.000000000000000000, 0.000000000000000000, 0.000000000000000000 ) ) ;
#1565=CARTESIAN_POINT ( 'NONE',  ( 17.15242344757784210, 8.297343789534778580, 4.632629386303498187 ) ) ;
#1567=ORIENTED_EDGE ( 'NONE', *, *, #13985, .T. ) ;
#1570=ORIENTED_EDGE ( 'NONE', *, *, #8432, .F. ) ;
#1571=ORIENTED_EDGE ( 'NONE', *, *, #1917, .T. ) ;
#1574=ORIENTED_EDGE ( 'NONE', *, *, #251, .T. ) ;
#1580=ADVANCED_FACE ( 'NONE', ( #632 ), #15227, .F. ) ;
#1584=ORIENTED_EDGE ( 'NONE', *, *, #16258, .F. ) ;
#1588=CARTESIAN_POINT ( 'NONE',  ( 41.99999999999999289, 25.93535998569253920, -27.00000000000000000 ) ) ;
#1595=CARTESIAN_POINT ( 'NONE',  ( -40.89823313241237912, -26.41789760203349502, 27.00000000000000000 ) ) ;
#1608=VECTOR ( 'NONE', #17271, 1000.000000000000000 ) ;
#1631=ORIENTED_EDGE ( 'NONE', *, *, #13899, .T. ) ;
#1632=EDGE_CURVE ( 'NONE', #8004, #8486, #5988, .T. ) ;
#1640=EDGE_CURVE ( 'NONE', #10789, #16240, #14868, .T. ) ;
#1643=ORIENTED_EDGE ( 'NONE', *, *, #19336, .T. ) ;
#1657=AXIS2_PLACEMENT_3D ( 'NONE', #22226, #8911, #23587 ) ;
#1678=CARTESIAN_POINT ( 'NONE',  ( 29.00000000000000711, -29.50000000000000711, -27.00000000000000000 ) ) ;
#1695=AXIS2_PLACEMENT_3D ( 'NONE', #14206, #13984, #2753 ) ;
#1701=CIRCLE ( 'NONE', #4421, 1.999999999999994449 ) ;
#1702=AXIS2_PLACEMENT_3D ( 'NONE', #16398, #12268, #3480 ) ;
#1705=CARTESIAN_POINT ( 'NONE',  ( -20.85000000000000142, -15.03999999999999915, -25.00000000000000000 ) ) ;
#1718=CARTESIAN_POINT ( 'NONE',  ( -14.99999999999999822, -6.045577542124163753E-21, 9.499999999999994671 ) ) ;
#1719=ORIENTED_EDGE ( 'NONE', *, *, #13137, .T. ) ;
#1722=AXIS2_PLACEMENT_3D ( 'NONE', #17393, #9685, #13358 ) ;
#1723=ORIENTED_EDGE ( 'NONE', *, *, #20066, .T. ) ;
#1726=DIRECTION ( 'NONE',  ( -1.000000000000000000, -0.000000000000000000, -0.000000000000000000 ) ) ;
#1728=EDGE_CURVE ( 'NONE', #3850, #13548, #17943, .T. ) ;
#1737=CIRCLE ( 'NONE', #2110, 1.999999999999994449 ) ;
#1741=DIRECTION ( 'NONE',  ( -1.000000000000000000, 0.000000000000000000, 0.000000000000000000 ) ) ;
#1745=EDGE_LOOP ( 'NONE', ( #9840, #20300, #22621, #13867 ) ) ;
#1753=EDGE_CURVE ( 'NONE', #8486, #23937, #21373, .T. ) ;
#1764=CARTESIAN_POINT ( 'NONE',  ( -14.51962751333974033, -3.765689428759031010, -8.721787840009202597 ) ) ;
#1798=CIRCLE ( 'NONE', #1414, 50.00000000000000000 ) ;
#1799=AXIS2_PLACEMENT_3D ( 'NONE', #5246, #12672, #12315 ) ;
#1805=CYLINDRICAL_SURFACE ( 'NONE', #12978, 14.99999999999999822 ) ;
#1806=CARTESIAN_POINT ( 'NONE',  ( 0.000000000000000000, 15.03999999999999915, 25.00000000000000000 ) ) ;
#1823=ORIENTED_EDGE ( 'NONE', *, *, #20698, .T. ) ;
#1828=DIRECTION ( 'NONE',  ( 0.000000000000000000, -1.000000000000000000, 0.000000000000000000 ) ) ;
#1830=EDGE_LOOP ( 'NONE', ( #19307, #11807, #13677, #13845 ) ) ;
#1833=CARTESIAN_POINT ( 'NONE',  ( -17.32141611691247718, 8.728455122802976973, -3.780491077225285768 ) ) ;
#1837=ADVANCED_FACE ( 'NONE', ( #9903 ), #7709, .F. ) ;
#1839=ORIENTED_EDGE ( 'NONE', *, *, #12777, .T. ) ;
#1840=DIRECTION ( 'NONE',  ( -0.000000000000000000, -0.000000000000000000, -1.000000000000000000 ) ) ;
#1846=FACE_OUTER_BOUND ( 'NONE', #6917, .T. ) ;
#1852=ORIENTED_EDGE ( 'NONE', *, *, #22143, .T. ) ;
#1860=FACE_OUTER_BOUND ( 'NONE', #23285, .T. ) ;
#1861=DIRECTION ( 'NONE',  ( -0.000000000000000000, -0.000000000000000000, 1.000000000000000000 ) ) ;
#1875=ADVANCED_FACE ( 'NONE', ( #14412 ), #23715, .F. ) ;
#1876=LINE ( 'NONE', #5666, #10993 ) ;
#1888=CARTESIAN_POINT ( 'NONE',  ( 15.78970982176773319, -5.581464347350856947, 7.700125654604338621 ) ) ;
#1891=ORIENTED_EDGE ( 'NONE', *, *, #13570, .F. ) ;
#1894=DIRECTION ( 'NONE',  ( 0.7071067811865660024, 8.659560562355159656E-17, -0.7071067811865291430 ) ) ;
#1902=CARTESIAN_POINT ( 'NONE',  ( 31.10231664966676135, 45.36128193761570770, 27.00000000000000000 ) ) ;
#1904=EDGE_LOOP ( 'NONE', ( #5054, #3375 ) ) ;
#1917=EDGE_CURVE ( 'NONE', #15957, #22631, #15895, .T. ) ;
#1919=CARTESIAN_POINT ( 'NONE',  ( 0.000000000000000000, -15.23000000000000220, -27.00000000000000000 ) ) ;
#1920=ORIENTED_EDGE ( 'NONE', *, *, #20741, .F. ) ;
#1933=CARTESIAN_POINT ( 'NONE',  ( -20.85000000000000142, -15.03999999999999915, 25.00000000000000000 ) ) ;
#1937=CARTESIAN_POINT ( 'NONE',  ( -17.52920230446416738, 9.315347328456301312, 1.925892650121555416 ) ) ;
#1944=CARTESIAN_POINT ( 'NONE',  ( -41.99999999999999289, 0.000000000000000000, 9.499999999999994671 ) ) ;
#1949=EDGE_CURVE ( 'NONE', #11857, #18226, #3197, .T. ) ;
#1958=DIRECTION ( 'NONE',  ( -0.000000000000000000, -0.000000000000000000, -1.000000000000000000 ) ) ;
#1960=VERTEX_POINT ( 'NONE', #10629 ) ;
#1987=DIRECTION ( 'NONE',  ( -1.000000000000000000, 0.000000000000000000, 0.000000000000000000 ) ) ;
#2000=SHAPE_DEFINITION_REPRESENTATION ( #14492, #8762 ) ;
#2001=EDGE_CURVE ( 'NONE', #14761, #14835, #8507, .T. ) ;
#2005=ADVANCED_FACE ( 'NONE', ( #18687 ), #9038, .F. ) ;
#2015=FACE_OUTER_BOUND ( 'NONE', #1402, .T. ) ;
#2043=DIRECTION ( 'NONE',  ( -0.000000000000000000, -0.000000000000000000, 1.000000000000000000 ) ) ;
#2050=ORIENTED_EDGE ( 'NONE', *, *, #7379, .T. ) ;
#2054=CARTESIAN_POINT ( 'NONE',  ( 20.84999999999999432, -15.04000000000000448, -27.00000000000000000 ) ) ;
#2056=CARTESIAN_POINT ( 'NONE',  ( -16.68233279685676607, 7.225448002938851033, -6.184784653374926222 ) ) ;
#2061=ORIENTED_EDGE ( 'NONE', *, *, #14810, .F. ) ;
#2069=VECTOR ( 'NONE', #15183, 999.9999999999998863 ) ;
#2075=DIRECTION ( 'NONE',  ( 4.613626265895764052E-16, 1.000000000000000000, 0.000000000000000000 ) ) ;
#2079=ORIENTED_EDGE ( 'NONE', *, *, #13110, .T. ) ;
#2083=CARTESIAN_POINT ( 'NONE',  ( 14.79187224938325151, 2.570168443617191212, -9.168425918763420057 ) ) ;
#2095=ORIENTED_EDGE ( 'NONE', *, *, #2766, .T. ) ;
#2100=EDGE_CURVE ( 'NONE', #1960, #17886, #2272, .T. ) ;
#2108=CARTESIAN_POINT ( 'NONE',  ( -20.85000000000000853, 15.04000000000000092, -27.00000000000000000 ) ) ;
#2110=AXIS2_PLACEMENT_3D ( 'NONE', #6982, #7333, #5149 ) ;
#2116=ORIENTED_EDGE ( 'NONE', *, *, #476, .F. ) ;
#2146=CARTESIAN_POINT ( 'NONE',  ( 0.000000000000000000, 45.00000000000000000, 27.00000000000000000 ) ) ;
#2147=DIRECTION ( 'NONE',  ( -1.000000000000000000, 0.000000000000000000, 0.000000000000000000 ) ) ;
#2151=VECTOR ( 'NONE', #23351, 1000.000000000000000 ) ;
#2152=ORIENTED_EDGE ( 'NONE', *, *, #6077, .T. ) ;
#2158=AXIS2_PLACEMENT_3D ( 'NONE', #12507, #8385, #23761 ) ;
#2162=DIRECTION ( 'NONE',  ( 0.000000000000000000, 0.000000000000000000, 1.000000000000000000 ) ) ;
#2163=ADVANCED_FACE ( 'NONE', ( #15491, #16965, #18935, #21112, #7922, #5866, #279, #20753 ), #22959, .T. ) ;
#2179=EDGE_CURVE ( 'NONE', #20131, #14640, #17307, .T. ) ;
#2181=AXIS2_PLACEMENT_3D ( 'NONE', #15805, #8353, #19362 ) ;
#2184=CARTESIAN_POINT ( 'NONE',  ( -15.09475045435787166, 4.494086555308239639, -8.407297576120608795 ) ) ;
#2199=DIRECTION ( 'NONE',  ( 1.000000000000000000, -0.000000000000000000, -0.000000000000000000 ) ) ;
#2209=DIRECTION ( 'NONE',  ( -1.000000000000000000, 0.000000000000000000, 0.000000000000000000 ) ) ;
#2216=DIRECTION ( 'NONE',  ( -0.000000000000000000, -0.000000000000000000, -1.000000000000000000 ) ) ;
#2220=VECTOR ( 'NONE', #8223, 1000.000000000000000 ) ;
#2222=VERTEX_POINT ( 'NONE', #16108 ) ;
#2225=LINE ( 'NONE', #17092, #22862 ) ;
#2226=DIRECTION ( 'NONE',  ( -0.000000000000000000, -0.000000000000000000, -1.000000000000000000 ) ) ;
#2227=ORIENTED_EDGE ( 'NONE', *, *, #2483, .F. ) ;
#2230=ORIENTED_EDGE ( 'NONE', *, *, #20570, .F. ) ;
#2231=DIRECTION ( 'NONE',  ( 1.000000000000000000, -0.000000000000000000, -0.000000000000000000 ) ) ;
#2238=DIRECTION ( 'NONE',  ( -1.000000000000000000, 0.000000000000000000, 0.000000000000000000 ) ) ;
#2239=EDGE_CURVE ( 'NONE', #760, #8771, #19898, .T. ) ;
#2252=CIRCLE ( 'NONE', #1107, 9.499999999999989342 ) ;
#2264=ORIENTED_EDGE ( 'NONE', *, *, #19666, .F. ) ;
#2267=DIRECTION ( 'NONE',  ( 0.000000000000000000, 0.000000000000000000, -1.000000000000000000 ) ) ;
#2271=PLANE ( 'NONE',  #6171 ) ;
#2272=CIRCLE ( 'NONE', #16691, 4.999999999999997335 ) ;
#2279=CARTESIAN_POINT ( 'NONE',  ( 41.99999999999999289, 5.618459588085056979E-15, -10.50249999999999950 ) ) ;
#2282=ORIENTED_EDGE ( 'NONE', *, *, #755, .T. ) ;
#2287=DIRECTION ( 'NONE',  ( -0.000000000000000000, -0.000000000000000000, -1.000000000000000000 ) ) ;
#2295=FACE_OUTER_BOUND ( 'NONE', #4589, .T. ) ;
#2311=ORIENTED_EDGE ( 'NONE', *, *, #15135, .F. ) ;
#2314=SHAPE_REPRESENTATION_RELATIONSHIP ( 'NONE' , 'NONE' ,  #8762, #17167 ) ;
#2321=LINE ( 'NONE', #19286, #18832 ) ;
#2344=AXIS2_PLACEMENT_3D ( 'NONE', #24063, #20287, #7341 ) ;
#2350=VERTEX_POINT ( 'NONE', #14751 ) ;
#2355=CARTESIAN_POINT ( 'NONE',  ( -28.99999999999999645, 29.50000000000000000, 27.00000000000000000 ) ) ;
#2370=EDGE_LOOP ( 'NONE', ( #21447, #11613, #15304, #20594 ) ) ;
#2380=CARTESIAN_POINT ( 'NONE',  ( 1.999999999999994449, 45.00000000000000000, 23.99999999999999645 ) ) ;
#2381=CARTESIAN_POINT ( 'NONE',  ( 29.00000000000000711, -29.50000000000000711, -27.00000000000000000 ) ) ;
#2394=EDGE_LOOP ( 'NONE', ( #1474, #1527, #23306, #8204, #12895, #6035, #13576, #8407, #13705 ) ) ;
#2406=FACE_OUTER_BOUND ( 'NONE', #9405, .T. ) ;
#2410=EDGE_LOOP ( 'NONE', ( #21868, #21107, #1584, #22497 ) ) ;
#2415=DIRECTION ( 'NONE',  ( -0.000000000000000000, -0.000000000000000000, 1.000000000000000000 ) ) ;
#2435=VECTOR ( 'NONE', #726, 1000.000000000000000 ) ;
#2448=CIRCLE ( 'NONE', #1695, 1.999999999999994449 ) ;
#2449=CARTESIAN_POINT ( 'NONE',  ( 0.000000000000000000, 0.000000000000000000, -27.00000000000000000 ) ) ;
#2460=DIRECTION ( 'NONE',  ( -0.000000000000000000, -0.000000000000000000, -1.000000000000000000 ) ) ;
#2462=ADVANCED_FACE ( 'NONE', ( #19872, #10388 ), #21937, .T. ) ;
#2463=EDGE_CURVE ( 'NONE', #20705, #4173, #13404, .T. ) ;
#2466=CYLINDRICAL_SURFACE ( 'NONE', #3774, 23.84999999999999432 ) ;
#2469=ORIENTED_EDGE ( 'NONE', *, *, #4120, .T. ) ;
#2473=CIRCLE ( 'NONE', #16880, 23.85000000000000497 ) ;
#2475=ORIENTED_EDGE ( 'NONE', *, *, #1632, .T. ) ;
#2478=AXIS2_PLACEMENT_3D ( 'NONE', #12357, #8572, #12236 ) ;
#2483=EDGE_CURVE ( 'NONE', #23403, #20131, #5085, .T. ) ;
#2494=EDGE_CURVE ( 'NONE', #16240, #13688, #17273, .T. ) ;
#2501=AXIS2_PLACEMENT_3D ( 'NONE', #3109, #5067, #12115 ) ;
#2502=CONICAL_SURFACE ( 'NONE', #23173, 2.024999999999999911, 0.7853981633974743692 ) ;
#2505=VERTEX_POINT ( 'NONE', #13504 ) ;
#2528=EDGE_LOOP ( 'NONE', ( #12554, #9189, #15368, #1567 ) ) ;
#2540=AXIS2_PLACEMENT_3D ( 'NONE', #9026, #20039, #21752 ) ;
#2542=PLANE ( 'NONE',  #14269 ) ;
#2548=VECTOR ( 'NONE', #19758, 1000.000000000000000 ) ;
#2557=DIRECTION ( 'NONE',  ( -1.000000000000000000, 0.000000000000000000, 0.000000000000000000 ) ) ;
#2564=AXIS2_PLACEMENT_3D ( 'NONE', #12487, #17767, #16278 ) ;
#2571=CARTESIAN_POINT ( 'NONE',  ( 41.49999999999999289, 27.79189783386526358, 27.00000000000000000 ) ) ;
#2583=DIRECTION ( 'NONE',  ( 0.000000000000000000, 0.000000000000000000, 1.000000000000000000 ) ) ;
#2604=CARTESIAN_POINT ( 'NONE',  ( -20.85000000000000853, 15.04000000000000092, 25.00000000000000000 ) ) ;
#2608=EDGE_CURVE ( 'NONE', #5686, #5827, #22792, .T. ) ;
#2619=VERTEX_POINT ( 'NONE', #8458 ) ;
#2620=CARTESIAN_POINT ( 'NONE',  ( -23.85000000000000497, 15.03999999999999915, -27.00000000000000000 ) ) ;
#2640=CARTESIAN_POINT ( 'NONE',  ( 0.000000000000000000, 45.00000000000000000, 27.00000000000000000 ) ) ;
#2646=CARTESIAN_POINT ( 'NONE',  ( -14.91624121966758487, -1.615102390220945150, 9.367332145225624629 ) ) ;
#2669=DIRECTION ( 'NONE',  ( -0.000000000000000000, -0.000000000000000000, -1.000000000000000000 ) ) ;
#2671=CIRCLE ( 'NONE', #14339, 1.500000000000001332 ) ;
#2676=VERTEX_POINT ( 'NONE', #2108 ) ;
#2686=CARTESIAN_POINT ( 'NONE',  ( 14.79227890392045452, -2.568991289487080554, -9.169086800441903051 ) ) ;
#2688=EDGE_CURVE ( 'NONE', #886, #2809, #9398, .T. ) ;
#2693=CARTESIAN_POINT ( 'NONE',  ( 0.000000000000000000, -45.00000000000000000, -23.99999999999999645 ) ) ;
#2698=DIRECTION ( 'NONE',  ( -0.000000000000000000, -0.000000000000000000, -1.000000000000000000 ) ) ;
#2701=AXIS2_PLACEMENT_3D ( 'NONE', #15454, #19381, #6194 ) ;
#2724=ORIENTED_EDGE ( 'NONE', *, *, #16561, .T. ) ;
#2725=DIRECTION ( 'NONE',  ( 1.000000000000000000, 0.000000000000000000, 0.000000000000000000 ) ) ;
#2732=FACE_OUTER_BOUND ( 'NONE', #10881, .T. ) ;
#2735=ORIENTED_EDGE ( 'NONE', *, *, #11602, .T. ) ;
#2742=EDGE_LOOP ( 'NONE', ( #14466, #22632, #9331, #5030 ) ) ;
#2745=CARTESIAN_POINT ( 'NONE',  ( 0.000000000000000000, 15.03999999999999915, 25.00000000000000000 ) ) ;
#2746=FACE_OUTER_BOUND ( 'NONE', #22864, .T. ) ;
#2748=CARTESIAN_POINT ( 'NONE',  ( -17.15849686392983386, -8.309918483244988607, -4.628645577532794597 ) ) ;
#2749=CARTESIAN_POINT ( 'NONE',  ( 18.50000000000000000, 15.23000000000000398, -27.00000000000000000 ) ) ;
#2753=DIRECTION ( 'NONE',  ( -1.000000000000000000, 0.000000000000000000, 0.000000000000000000 ) ) ;
#2756=CARTESIAN_POINT ( 'NONE',  ( -14.99999999999999822, -6.045577542124163753E-21, 9.499999999999994671 ) ) ;
#2758=FACE_OUTER_BOUND ( 'NONE', #22913, .T. ) ;
#2761=EDGE_CURVE ( 'NONE', #6272, #20027, #9911, .T. ) ;
#2766=EDGE_CURVE ( 'NONE', #17283, #22874, #8152, .T. ) ;
#2775=UNCERTAINTY_MEASURE_WITH_UNIT (LENGTH_MEASURE( 1.000000000000000082E-05 ), #14153, 'distance_accuracy_value', 'NONE');
#2776=CONICAL_SURFACE ( 'NONE', #22642, 2.024999999999999911, 0.7853981633974743692 ) ;
#2781=DIRECTION ( 'NONE',  ( 1.000000000000000000, 0.000000000000000000, 0.000000000000000000 ) ) ;
#2785=FACE_OUTER_BOUND ( 'NONE', #16371, .T. ) ;
#2786=DIRECTION ( 'NONE',  ( -1.000000000000000000, 0.000000000000000000, 0.000000000000000000 ) ) ;
#2788=VECTOR ( 'NONE', #10640, 1000.000000000000000 ) ;
#2789=LINE ( 'NONE', #4524, #3292 ) ;
#2790=VERTEX_POINT ( 'NONE', #4902 ) ;
#2791=AXIS2_PLACEMENT_3D ( 'NONE', #3801, #18100, #8812 ) ;
#2795=EDGE_LOOP ( 'NONE', ( #19708, #12776 ) ) ;
#2798=EDGE_CURVE ( 'NONE', #7541, #3277, #9957, .T. ) ;
#2800=CARTESIAN_POINT ( 'NONE',  ( 40.89823313241237912, 26.41789760203348081, 27.00000000000000000 ) ) ;
#2805=CARTESIAN_POINT ( 'NONE',  ( 15.00000000000000000, 6.781880092842756171E-15, 9.499999999999987566 ) ) ;
#2809=VERTEX_POINT ( 'NONE', #10830 ) ;
#2819=CARTESIAN_POINT ( 'NONE',  ( 0.000000000000000000, -45.00000000000000000, -23.99999999999999645 ) ) ;
#2825=AXIS2_PLACEMENT_3D ( 'NONE', #19395, #2669, #15580 ) ;
#2826=EDGE_CURVE ( 'NONE', #20997, #13001, #16443, .T. ) ;
#2836=AXIS2_PLACEMENT_3D ( 'NONE', #966, #19635, #10340 ) ;
#2840=AXIS2_PLACEMENT_3D ( 'NONE', #11523, #18993, #2267 ) ;
#2867=CARTESIAN_POINT ( 'NONE',  ( 0.000000000000000000, 45.00000000000000000, -23.99999999999999645 ) ) ;
#2872=CARTESIAN_POINT ( 'NONE',  ( -28.99999999999999645, -29.50000000000001066, -27.00000000000000000 ) ) ;
#2881=LINE ( 'NONE', #9803, #2220 ) ;
#2884=CARTESIAN_POINT ( 'NONE',  ( 16.81886298599061291, -7.518780870797755256, -5.825851398835375505 ) ) ;
#2891=CIRCLE ( 'NONE', #16514, 5.100000000000000533 ) ;
#2902=AXIS2_PLACEMENT_3D ( 'NONE', #16552, #7286, #14830 ) ;
#2917=CARTESIAN_POINT ( 'NONE',  ( -1.999999999999994449, -45.00000000000000000, -23.99999999999999645 ) ) ;
#2918=DIRECTION ( 'NONE',  ( 0.000000000000000000, 0.000000000000000000, 1.000000000000000000 ) ) ;
#2931=LINE ( 'NONE', #6474, #6063 ) ;
#2934=AXIS2_PLACEMENT_3D ( 'NONE', #233, #19255, #5829 ) ;
#2940=EDGE_LOOP ( 'NONE', ( #12955, #17330, #17250, #12060 ) ) ;
#2946=AXIS2_PLACEMENT_3D ( 'NONE', #20778, #13687, #4069 ) ;
#2949=CONICAL_SURFACE ( 'NONE', #6060, 1.999999999999994449, 1.029744258676653201 ) ;
#2950=CARTESIAN_POINT ( 'NONE',  ( -14.51962751333974389, 3.765689428759031010, 27.00000000000000000 ) ) ;
#2953=DIRECTION ( 'NONE',  ( 0.000000000000000000, 0.000000000000000000, -1.000000000000000000 ) ) ;
#2959=CARTESIAN_POINT ( 'NONE',  ( 29.00000000000000355, 29.50000000000000000, 27.00000000000000000 ) ) ;
#2964=CIRCLE ( 'NONE', #5694, 18.49999999999999645 ) ;
#2989=DIRECTION ( 'NONE',  ( -1.000000000000000000, 0.000000000000000000, 0.000000000000000000 ) ) ;
#2998=CARTESIAN_POINT ( 'NONE',  ( -20.85000000000000853, -15.03999999999999559, 25.00000000000000000 ) ) ;
#3013=LINE ( 'NONE', #16171, #21435 ) ;
#3016=CARTESIAN_POINT ( 'NONE',  ( 15.09475045435787877, -4.494086555308249409, -8.407297576120592808 ) ) ;
#3020=ORIENTED_EDGE ( 'NONE', *, *, #10934, .F. ) ;
#3021=DIRECTION ( 'NONE',  ( 0.000000000000000000, 0.000000000000000000, 1.000000000000000000 ) ) ;
#3040=CARTESIAN_POINT ( 'NONE',  ( 40.00000000000000711, 29.50000000000000000, 27.00000000000000000 ) ) ;
#3047=VERTEX_POINT ( 'NONE', #20968 ) ;
#3063=ORIENTED_EDGE ( 'NONE', *, *, #22143, .F. ) ;
#3103=CIRCLE ( 'NONE', #19484, 1.999999999999994449 ) ;
#3107=FACE_OUTER_BOUND ( 'NONE', #10013, .T. ) ;
#3109=CARTESIAN_POINT ( 'NONE',  ( 0.000000000000000000, -45.00000000000000000, -27.00000000000000000 ) ) ;
#3115=ADVANCED_FACE ( 'NONE', ( #959 ), #14349, .F. ) ;
#3119=CARTESIAN_POINT ( 'NONE',  ( 17.05196227081077254, -8.053793831531459446, -5.044162359773890714 ) ) ;
#3122=EDGE_CURVE ( 'NONE', #4244, #19649, #1397, .T. ) ;
#3125=CARTESIAN_POINT ( 'NONE',  ( 39.99999999999999289, 27.79189783386526358, -27.00000000000000000 ) ) ;
#3132=EDGE_LOOP ( 'NONE', ( #20937, #14012, #9678, #21947, #2227, #6144 ) ) ;
#3135=AXIS2_PLACEMENT_3D ( 'NONE', #23219, #3513, #23892 ) ;
#3139=DIRECTION ( 'NONE',  ( -0.000000000000000000, -0.000000000000000000, -1.000000000000000000 ) ) ;
#3143=ADVANCED_FACE ( 'NONE', ( #15950 ), #23529, .F. ) ;
#3144=CYLINDRICAL_SURFACE ( 'NONE', #18011, 20.85000000000000142 ) ;
#3147=CARTESIAN_POINT ( 'NONE',  ( 17.59041996266972774, 9.500503876990125107, -0.4759723220310729253 ) ) ;
#3164=CARTESIAN_POINT ( 'NONE',  ( 23.85000000000000497, 15.03999999999999915, -25.00000000000000000 ) ) ;
#3165=VERTEX_POINT ( 'NONE', #18157 ) ;
#3175=EDGE_CURVE ( 'NONE', #3699, #12983, #1455, .T. ) ;
#3180=DIRECTION ( 'NONE',  ( -0.7071067811865660024, 0.000000000000000000, -0.7071067811865291430 ) ) ;
#3186=DIRECTION ( 'NONE',  ( 0.000000000000000000, 0.000000000000000000, -1.000000000000000000 ) ) ;
#3197=LINE ( 'NONE', #17972, #19813 ) ;
#3203=EDGE_LOOP ( 'NONE', ( #20408, #13044, #12806 ) ) ;
#3207=DIRECTION ( 'NONE',  ( -0.000000000000000000, -0.000000000000000000, 1.000000000000000000 ) ) ;
#3221=AXIS2_PLACEMENT_3D ( 'NONE', #14541, #22008, #5287 ) ;
#3239=CARTESIAN_POINT ( 'NONE',  ( 15.56475192642548500, -5.220978644676161018, 7.947934502462929096 ) ) ;
#3259=DIRECTION ( 'NONE',  ( -0.000000000000000000, -0.000000000000000000, -1.000000000000000000 ) ) ;
#3265=ORIENTED_EDGE ( 'NONE', *, *, #14687, .T. ) ;
#3269=FACE_OUTER_BOUND ( 'NONE', #2940, .T. ) ;
#3277=VERTEX_POINT ( 'NONE', #7278 ) ;
#3292=VECTOR ( 'NONE', #8262, 1000.000000000000000 ) ;
#3308=CARTESIAN_POINT ( 'NONE',  ( 0.000000000000000000, -45.00000000000000000, 26.97499999999999432 ) ) ;
#3313=DIRECTION ( 'NONE',  ( 1.000000000000000000, 0.000000000000000000, 0.000000000000000000 ) ) ;
#3316=FACE_BOUND ( 'NONE', #1904, .T. ) ;
#3322=CARTESIAN_POINT ( 'NONE',  ( 40.00000000000000000, -29.50000000000000000, 27.00000000000000000 ) ) ;
#3323=ADVANCED_FACE ( 'NONE', ( #2015 ), #7619, .F. ) ;
#3326=ORIENTED_EDGE ( 'NONE', *, *, #14060, .F. ) ;
#3338=DIRECTION ( 'NONE',  ( -1.000000000000000000, 0.000000000000000000, 0.000000000000000000 ) ) ;
#3342=CIRCLE ( 'NONE', #7216, 20.85000000000000142 ) ;
#3360=CYLINDRICAL_SURFACE ( 'NONE', #16723, 1.999999999999994449 ) ;
#3362=CARTESIAN_POINT ( 'NONE',  ( 16.19099482616364227, -6.271157271432196367, 7.149633965064770003 ) ) ;
#3375=ORIENTED_EDGE ( 'NONE', *, *, #4061, .F. ) ;
#3378=DIRECTION ( 'NONE',  ( -0.000000000000000000, -0.000000000000000000, 1.000000000000000000 ) ) ;
#3385=DIRECTION ( 'NONE',  ( -0.000000000000000000, -0.000000000000000000, -1.000000000000000000 ) ) ;
#3392=DIRECTION ( 'NONE',  ( 0.000000000000000000, 0.000000000000000000, 1.000000000000000000 ) ) ;
#3394=CARTESIAN_POINT ( 'NONE',  ( 17.52920230446416738, 9.315347328456299536, -1.925892650121554750 ) ) ;
#3400=ORIENTED_EDGE ( 'NONE', *, *, #2001, .T. ) ;
#3405=DIRECTION ( 'NONE',  ( -1.000000000000000000, 0.000000000000000000, 0.000000000000000000 ) ) ;
#3411=ADVANCED_FACE ( 'NONE', ( #12822 ), #12710, .T. ) ;
#3412=EDGE_CURVE ( 'NONE', #19649, #4244, #7680, .T. ) ;
#3415=LINE ( 'NONE', #3526, #7861 ) ;
#3417=EDGE_LOOP ( 'NONE', ( #18996, #14497, #21570, #23141 ) ) ;
#3426=AXIS2_PLACEMENT_3D ( 'NONE', #10404, #3259, #20331 ) ;
#3427=CARTESIAN_POINT ( 'NONE',  ( -14.51962751333974033, -3.765689428759031010, 27.00000000000000000 ) ) ;
#3434=ORIENTED_EDGE ( 'NONE', *, *, #13022, .T. ) ;
#3435=FACE_BOUND ( 'NONE', #14343, .T. ) ;
#3436=LINE ( 'NONE', #18319, #8661 ) ;
#3447=ORIENTED_EDGE ( 'NONE', *, *, #8924, .T. ) ;
#3479=EDGE_CURVE ( 'NONE', #6633, #20997, #8083, .T. ) ;
#3480=DIRECTION ( 'NONE',  ( -1.000000000000000000, 0.000000000000000000, 0.000000000000000000 ) ) ;
#3485=ORIENTED_EDGE ( 'NONE', *, *, #1632, .F. ) ;
#3489=ORIENTED_EDGE ( 'NONE', *, *, #8439, .F. ) ;
#3499=EDGE_CURVE ( 'NONE', #14835, #14761, #2252, .T. ) ;
#3500=ORIENTED_EDGE ( 'NONE', *, *, #9756, .F. ) ;
#3504=DIRECTION ( 'NONE',  ( 1.000000000000000000, 0.000000000000000000, 0.000000000000000000 ) ) ;
#3513=DIRECTION ( 'NONE',  ( -0.000000000000000000, -0.000000000000000000, 1.000000000000000000 ) ) ;
#3521=CARTESIAN_POINT ( 'NONE',  ( -41.99999999999999289, 0.000000000000000000, 0.000000000000000000 ) ) ;
#3526=CARTESIAN_POINT ( 'NONE',  ( -14.51962751333974033, -3.765689428759031010, 27.00000000000000000 ) ) ;
#3527=LINE ( 'NONE', #1933, #6711 ) ;
#3530=CARTESIAN_POINT ( 'NONE',  ( -40.89823313241237912, 26.41789760203348081, 27.00000000000000000 ) ) ;
#3539=DIRECTION ( 'NONE',  ( 0.7071067811865660024, 0.000000000000000000, 0.7071067811865291430 ) ) ;
#3551=ORIENTED_EDGE ( 'NONE', *, *, #21387, .F. ) ;
#3569=ORIENTED_EDGE ( 'NONE', *, *, #19604, .F. ) ;
#3572=EDGE_CURVE ( 'NONE', #18241, #11779, #22158, .T. ) ;
#3574=EDGE_LOOP ( 'NONE', ( #13850, #18168, #6301, #1574 ) ) ;
#3579=DIRECTION ( 'NONE',  ( -0.000000000000000000, -0.000000000000000000, -1.000000000000000000 ) ) ;
#3580=VECTOR ( 'NONE', #4283, 1000.000000000000000 ) ;
#3588=CARTESIAN_POINT ( 'NONE',  ( 14.80736872429922002, -4.130115634539738068, 8.564444421911355576 ) ) ;
#3622=CARTESIAN_POINT ( 'NONE',  ( 34.10000000000000853, 29.50000000000000000, -27.00000000000000000 ) ) ;
#3634=ORIENTED_EDGE ( 'NONE', *, *, #19149, .T. ) ;
#3646=CARTESIAN_POINT ( 'NONE',  ( -23.85000000000000497, 15.03999999999999915, 25.00000000000000000 ) ) ;
#3647=EDGE_CURVE ( 'NONE', #15990, #19865, #327, .T. ) ;
#3661=CIRCLE ( 'NONE', #20029, 5.100000000000000533 ) ;
#3663=CARTESIAN_POINT ( 'NONE',  ( -34.10000000000000142, 29.50000000000000000, 27.00000000000000000 ) ) ;
#3665=DIRECTION ( 'NONE',  ( -0.000000000000000000, -0.000000000000000000, -1.000000000000000000 ) ) ;
#3669=EDGE_CURVE ( 'NONE', #5827, #5686, #24085, .T. ) ;
#3673=CARTESIAN_POINT ( 'NONE',  ( -20.85000000000000853, -15.03999999999999737, 27.00000000000000000 ) ) ;
#3674=ADVANCED_FACE ( 'NONE', ( #22641 ), #2271, .F. ) ;
#3675=EDGE_CURVE ( 'NONE', #14640, #14835, #9440, .T. ) ;
#3679=ORIENTED_EDGE ( 'NONE', *, *, #13363, .T. ) ;
#3688=DIRECTION ( 'NONE',  ( -0.000000000000000000, -0.000000000000000000, -1.000000000000000000 ) ) ;
#3692=CARTESIAN_POINT ( 'NONE',  ( 2.024999999999999911, 45.00000000000000000, 27.00000000000000000 ) ) ;
#3699=VERTEX_POINT ( 'NONE', #328 ) ;
#3707=EDGE_CURVE ( 'NONE', #11452, #13972, #6570, .T. ) ;
#3718=AXIS2_PLACEMENT_3D ( 'NONE', #17221, #2231, #15392 ) ;
#3725=CARTESIAN_POINT ( 'NONE',  ( -20.85000000000000853, 15.04000000000000092, -27.00000000000000000 ) ) ;
#3745=CARTESIAN_POINT ( 'NONE',  ( 0.000000000000000000, -45.00000000000000000, 23.99999999999999645 ) ) ;
#3756=LINE ( 'NONE', #2279, #21163 ) ;
#3758=AXIS2_PLACEMENT_3D ( 'NONE', #20454, #18507, #9323 ) ;
#3774=AXIS2_PLACEMENT_3D ( 'NONE', #19312, #4671, #1135 ) ;
#3779=LINE ( 'NONE', #12798, #23143 ) ;
#3790=CARTESIAN_POINT ( 'NONE',  ( -41.49999999999999289, 27.79189783386526358, -27.00000000000000000 ) ) ;
#3801=CARTESIAN_POINT ( 'NONE',  ( 0.000000000000000000, 15.23000000000000220, 27.00000000000000000 ) ) ;
#3805=ORIENTED_EDGE ( 'NONE', *, *, #4003, .F. ) ;
#3808=ADVANCED_FACE ( 'NONE', ( #12119 ), #16035, .T. ) ;
#3814=EDGE_CURVE ( 'NONE', #5416, #569, #5825, .T. ) ;
#3818=LINE ( 'NONE', #11473, #4399 ) ;
#3821=AXIS2_PLACEMENT_3D ( 'NONE', #10512, #2725, #5050 ) ;
#3830=DIRECTION ( 'NONE',  ( -0.000000000000000000, -0.000000000000000000, -1.000000000000000000 ) ) ;
#3831=ADVANCED_FACE ( 'NONE', ( #21311 ), #8343, .F. ) ;
#3836=CARTESIAN_POINT ( 'NONE',  ( 1.999999999999994449, 45.00000000000000000, 23.99999999999999645 ) ) ;
#3838=EDGE_LOOP ( 'NONE', ( #19352, #5352, #15020, #1342 ) ) ;
#3846=ORIENTED_EDGE ( 'NONE', *, *, #10438, .F. ) ;
#3850=VERTEX_POINT ( 'NONE', #12737 ) ;
#3861=EDGE_LOOP ( 'NONE', ( #11961, #6796, #7209, #13340 ) ) ;
#3863=EDGE_LOOP ( 'NONE', ( #13655, #6070, #18703, #1852 ) ) ;
#3869=DIRECTION ( 'NONE',  ( 0.7071067811865500152, 0.000000000000000000, -0.7071067811865450192 ) ) ;
#3872=ORIENTED_EDGE ( 'NONE', *, *, #15324, .T. ) ;
#3883=DIRECTION ( 'NONE',  ( 1.000000000000000000, 0.000000000000000000, 0.000000000000000000 ) ) ;
#3887=VERTEX_POINT ( 'NONE', #11000 ) ;
#3888=EDGE_CURVE ( 'NONE', #3699, #10247, #14694, .T. ) ;
#3891=CARTESIAN_POINT ( 'NONE',  ( -17.06033556854818656, 8.068938288216804366, 5.036196554528638458 ) ) ;
#3894=VERTEX_POINT ( 'NONE', #8715 ) ;
#3934=DIRECTION ( 'NONE',  ( 0.9160001545545232160, 0.4011779117250717785, 0.000000000000000000 ) ) ;
#3935=CARTESIAN_POINT ( 'NONE',  ( -2.024999999999999911, 45.00000000000000000, 27.00000000000000000 ) ) ;
#3938=ORIENTED_EDGE ( 'NONE', *, *, #18494, .F. ) ;
#3977=CARTESIAN_POINT ( 'NONE',  ( 0.000000000000000000, 15.23000000000000220, 27.00000000000000000 ) ) ;
#3987=VECTOR ( 'NONE', #6394, 1000.000000000000000 ) ;
#3994=CYLINDRICAL_SURFACE ( 'NONE', #14222, 1.999999999999994449 ) ;
#4003=EDGE_CURVE ( 'NONE', #13451, #4173, #14322, .T. ) ;
#4004=CIRCLE ( 'NONE', #9426, 20.85000000000000142 ) ;
#4012=AXIS2_PLACEMENT_3D ( 'NONE', #5914, #15536, #4101 ) ;
#4025=ORIENTED_EDGE ( 'NONE', *, *, #2688, .F. ) ;
#4031=EDGE_CURVE ( 'NONE', #19513, #11779, #7815, .T. ) ;
#4041=DIRECTION ( 'NONE',  ( 1.000000000000000000, 0.000000000000000000, 0.000000000000000000 ) ) ;
#4048=CIRCLE ( 'NONE', #13393, 18.50000000000000000 ) ;
#4057=DIRECTION ( 'NONE',  ( -1.000000000000000000, 0.000000000000000000, 0.000000000000000000 ) ) ;
#4061=EDGE_CURVE ( 'NONE', #14, #10814, #22934, .T. ) ;
#4069=DIRECTION ( 'NONE',  ( -1.000000000000000000, 0.000000000000000000, 0.000000000000000000 ) ) ;
#4070=AXIS2_PLACEMENT_3D ( 'NONE', #2640, #10051, #4602 ) ;
#4080=DIRECTION ( 'NONE',  ( -1.000000000000000000, 0.000000000000000000, 0.000000000000000000 ) ) ;
#4081=CARTESIAN_POINT ( 'NONE',  ( 29.00000000000000711, -29.50000000000000711, 27.00000000000000000 ) ) ;
#4095=VERTEX_POINT ( 'NONE', #19077 ) ;
#4101=DIRECTION ( 'NONE',  ( 1.000000000000000000, 0.000000000000000000, 0.000000000000000000 ) ) ;
#4106=FACE_OUTER_BOUND ( 'NONE', #3132, .T. ) ;
#4112=AXIS2_PLACEMENT_3D ( 'NONE', #20625, #11447, #18925 ) ;
#4116=FACE_OUTER_BOUND ( 'NONE', #6757, .T. ) ;
#4117=CARTESIAN_POINT ( 'NONE',  ( 15.78970982176773674, 5.581464347350856059, -7.700125654604351055 ) ) ;
#4120=EDGE_CURVE ( 'NONE', #4095, #19404, #2671, .T. ) ;
#4121=LINE ( 'NONE', #13506, #22018 ) ;
#4132=CARTESIAN_POINT ( 'NONE',  ( 0.000000000000000000, -45.00000000000000000, 27.00000000000000000 ) ) ;
#4139=CARTESIAN_POINT ( 'NONE',  ( 0.000000000000000000, -15.03999999999999915, 27.00000000000000000 ) ) ;
#4173=VERTEX_POINT ( 'NONE', #20555 ) ;
#4185=DIRECTION ( 'NONE',  ( 0.000000000000000000, 0.000000000000000000, 1.000000000000000000 ) ) ;
#4187=EDGE_LOOP ( 'NONE', ( #19519, #7340, #15155, #7051, #4359, #19941 ) ) ;
#4193=ORIENTED_EDGE ( 'NONE', *, *, #6657, .F. ) ;
#4199=CARTESIAN_POINT ( 'NONE',  ( -30.44534269664590198, -40.40463133211081015, 27.00000000000000000 ) ) ;
#4210=ORIENTED_EDGE ( 'NONE', *, *, #7673, .T. ) ;
#4223=ORIENTED_EDGE ( 'NONE', *, *, #2826, .F. ) ;
#4229=CARTESIAN_POINT ( 'NONE',  ( 31.10231664966676135, 45.36128193761570770, -27.00000000000000000 ) ) ;
#4235=CARTESIAN_POINT ( 'NONE',  ( -30.44534269664590198, 40.40463133211079594, -27.00000000000000000 ) ) ;
#4244=VERTEX_POINT ( 'NONE', #21139 ) ;
#4246=CARTESIAN_POINT ( 'NONE',  ( -23.84999999999999432, -15.03999999999999915, 25.00000000000000000 ) ) ;
#4257=CARTESIAN_POINT ( 'NONE',  ( -28.99999999999999645, -29.50000000000001066, 27.00000000000000000 ) ) ;
#4262=EDGE_CURVE ( 'NONE', #20648, #18900, #15775, .T. ) ;
#4266=EDGE_CURVE ( 'NONE', #760, #11663, #3661, .T. ) ;
#4267=DIRECTION ( 'NONE',  ( -0.000000000000000000, -0.000000000000000000, -1.000000000000000000 ) ) ;
#4280=FACE_OUTER_BOUND ( 'NONE', #21379, .T. ) ;
#4283=DIRECTION ( 'NONE',  ( -0.000000000000000000, -0.000000000000000000, 1.000000000000000000 ) ) ;
#4317=CARTESIAN_POINT ( 'NONE',  ( -18.49999999999999645, -15.23000000000000220, 27.00000000000000000 ) ) ;
#4358=ORIENTED_EDGE ( 'NONE', *, *, #18640, .F. ) ;
#4359=ORIENTED_EDGE ( 'NONE', *, *, #3675, .T. ) ;
#4367=LINE ( 'NONE', #713, #18520 ) ;
#4399=VECTOR ( 'NONE', #2226, 1000.000000000000000 ) ;
#4415=CARTESIAN_POINT ( 'NONE',  ( 14.51962751333974389, 3.765689428759031010, -8.721787840009197268 ) ) ;
#4417=CARTESIAN_POINT ( 'NONE',  ( 34.10000000000001563, -29.50000000000000711, -27.00000000000000000 ) ) ;
#4420=CARTESIAN_POINT ( 'NONE',  ( 42.00000000000000000, -25.93535998569253920, -27.00000000000000000 ) ) ;
#4421=AXIS2_PLACEMENT_3D ( 'NONE', #10652, #1172, #10423 ) ;
#4422=CARTESIAN_POINT ( 'NONE',  ( 41.99999999999999289, 5.618459588085056979E-15, 0.000000000000000000 ) ) ;
#4426=ORIENTED_EDGE ( 'NONE', *, *, #14171, .F. ) ;
#4443=CARTESIAN_POINT ( 'NONE',  ( -2.024999999999999911, -45.00000000000000000, -27.00000000000000000 ) ) ;
#4450=FACE_OUTER_BOUND ( 'NONE', #6189, .T. ) ;
#4461=ORIENTED_EDGE ( 'NONE', *, *, #3814, .T. ) ;
#4462=AXIS2_PLACEMENT_3D ( 'NONE', #17217, #765, #15617 ) ;
#4474=ORIENTED_EDGE ( 'NONE', *, *, #8144, .T. ) ;
#4481=CARTESIAN_POINT ( 'NONE',  ( -41.99999999999999289, 0.000000000000000000, 0.000000000000000000 ) ) ;
#4490=CARTESIAN_POINT ( 'NONE',  ( 16.82499651802897134, -7.532250541895347595, 5.808290850931478566 ) ) ;
#4493=EDGE_CURVE ( 'NONE', #13963, #9227, #9893, .T. ) ;
#4500=EDGE_CURVE ( 'NONE', #16347, #22742, #5598, .T. ) ;
#4508=DIRECTION ( 'NONE',  ( 1.000000000000000000, 0.000000000000000000, 0.000000000000000000 ) ) ;
#4509=DIRECTION ( 'NONE',  ( -0.000000000000000000, -0.000000000000000000, 1.000000000000000000 ) ) ;
#4523=CARTESIAN_POINT ( 'NONE',  ( -15.07341617659254496, 4.495283618570410589, 8.379779594489216166 ) ) ;
#4524=CARTESIAN_POINT ( 'NONE',  ( -28.27483331787890819, -41.23752903419608629, 27.00000000000000000 ) ) ;
#4529=VERTEX_POINT ( 'NONE', #23495 ) ;
#4531=CARTESIAN_POINT ( 'NONE',  ( 2.024999999999999911, -45.00000000000000000, -27.00000000000000000 ) ) ;
#4541=DIRECTION ( 'NONE',  ( 0.000000000000000000, -1.000000000000000000, 0.000000000000000000 ) ) ;
#4547=DIRECTION ( 'NONE',  ( -1.000000000000000000, 0.000000000000000000, 0.000000000000000000 ) ) ;
#4553=DIRECTION ( 'NONE',  ( 1.000000000000000000, 0.000000000000000000, 0.000000000000000000 ) ) ;
#4555=ORIENTED_EDGE ( 'NONE', *, *, #8377, .F. ) ;
#4562=PRODUCT_DEFINITION_FORMATION_WITH_SPECIFIED_SOURCE ( 'ANY', '', #19570, .NOT_KNOWN. ) ;
#4568=EDGE_CURVE ( 'NONE', #8063, #22874, #10771, .T. ) ;
#4575=EDGE_CURVE ( 'NONE', #20997, #19575, #10270, .T. ) ;
#4589=EDGE_LOOP ( 'NONE', ( #8654, #14665, #12030, #2475 ) ) ;
#4599=CARTESIAN_POINT ( 'NONE',  ( -17.49232137458054837, -9.205685982891289143, -2.395442301836272492 ) ) ;
#4602=DIRECTION ( 'NONE',  ( 1.000000000000000000, 0.000000000000000000, 0.000000000000000000 ) ) ;
#4609=DIRECTION ( 'NONE',  ( -0.000000000000000000, -0.000000000000000000, -1.000000000000000000 ) ) ;
#4610=CARTESIAN_POINT ( 'NONE',  ( 17.15242344757783499, -8.297343789534773251, -4.632629386303490193 ) ) ;
#4630=DIRECTION ( 'NONE',  ( -1.000000000000000000, 0.000000000000000000, 0.000000000000000000 ) ) ;
#4631=FACE_BOUND ( 'NONE', #20657, .T. ) ;
#4650=LINE ( 'NONE', #23680, #18554 ) ;
#4652=EDGE_CURVE ( 'NONE', #23565, #14989, #11417, .T. ) ;
#4653=CARTESIAN_POINT ( 'NONE',  ( 14.51962751333974211, -3.765689428759034563, -8.721787840009190163 ) ) ;
#4654=CARTESIAN_POINT ( 'NONE',  ( 41.99999999999999289, 25.93535998569253920, -27.00000000000000000 ) ) ;
#4655=EDGE_CURVE ( 'NONE', #10789, #22991, #23, .T. ) ;
#4658=EDGE_LOOP ( 'NONE', ( #12108, #18010, #13287, #23444 ) ) ;
#4666=EDGE_LOOP ( 'NONE', ( #16735, #6778, #2061, #17543 ) ) ;
#4671=DIRECTION ( 'NONE',  ( -0.000000000000000000, -0.000000000000000000, 1.000000000000000000 ) ) ;
#4684=CIRCLE ( 'NONE', #15953, 2.024999999999999911 ) ;
#4686=DIRECTION ( 'NONE',  ( -0.000000000000000000, -0.000000000000000000, -1.000000000000000000 ) ) ;
#4689=DIRECTION ( 'NONE',  ( 1.000000000000000000, 0.000000000000000000, 0.000000000000000000 ) ) ;
#4695=DIRECTION ( 'NONE',  ( -1.000000000000000000, 0.000000000000000000, 0.000000000000000000 ) ) ;
#4702=VERTEX_POINT ( 'NONE', #23349 ) ;
#4706=ADVANCED_FACE ( 'NONE', ( #17466 ), #6808, .F. ) ;
#4708=EDGE_CURVE ( 'NONE', #11663, #760, #21995, .T. ) ;
#4709=DIRECTION ( 'NONE',  ( 1.000000000000000000, 0.000000000000000000, 0.000000000000000000 ) ) ;
#4712=CARTESIAN_POINT ( 'NONE',  ( -17.59041996266973129, -9.500503876990130436, -0.4759723220310695391 ) ) ;
#4720=DIRECTION ( 'NONE',  ( -1.000000000000000000, 0.000000000000000000, 0.000000000000000000 ) ) ;
#4725=CARTESIAN_POINT ( 'NONE',  ( 14.67173559926287929, 3.179195828807838353, 8.975010320294691368 ) ) ;
#4735=CIRCLE ( 'NONE', #18354, 10.99999999999999645 ) ;
#4738=EDGE_CURVE ( 'NONE', #20131, #23091, #12449, .T. ) ;
#4745=DIRECTION ( 'NONE',  ( 1.000000000000000000, -4.613626265895764052E-16, 0.000000000000000000 ) ) ;
#4746=DIRECTION ( 'NONE',  ( -0.000000000000000000, -0.000000000000000000, -1.000000000000000000 ) ) ;
#4755=CYLINDRICAL_SURFACE ( 'NONE', #18824, 23.85000000000000497 ) ;
#4756=FACE_OUTER_BOUND ( 'NONE', #14452, .T. ) ;
#4781=CYLINDRICAL_SURFACE ( 'NONE', #21138, 5.100000000000000533 ) ;
#4792=LINE ( 'NONE', #10607, #15263 ) ;
#4828=DIRECTION ( 'NONE',  ( -0.000000000000000000, -0.000000000000000000, -1.000000000000000000 ) ) ;
#4836=CIRCLE ( 'NONE', #2478, 14.99999999999999822 ) ;
#4842=CARTESIAN_POINT ( 'NONE',  ( -16.68233279685676607, -7.225448002938850145, 6.184784653374924446 ) ) ;
#4857=FACE_OUTER_BOUND ( 'NONE', #3861, .T. ) ;
#4860=EDGE_LOOP ( 'NONE', ( #4025, #12431, #8164, #982 ) ) ;
#4883=DIRECTION ( 'NONE',  ( 1.000000000000000000, 0.000000000000000000, 0.000000000000000000 ) ) ;
#4902=CARTESIAN_POINT ( 'NONE',  ( -14.99999999999999822, 0.000000000000000000, -27.00000000000000000 ) ) ;
#4903=CARTESIAN_POINT ( 'NONE',  ( -40.89823313241237912, -26.41789760203349502, -27.00000000000000000 ) ) ;
#4905=EDGE_CURVE ( 'NONE', #498, #6272, #9978, .T. ) ;
#4906=EDGE_LOOP ( 'NONE', ( #12601, #23933, #1457, #12156 ) ) ;
#4907=DIRECTION ( 'NONE',  ( -0.000000000000000000, -0.000000000000000000, -1.000000000000000000 ) ) ;
#4916=ORIENTED_EDGE ( 'NONE', *, *, #11662, .F. ) ;
#4929=CARTESIAN_POINT ( 'NONE',  ( 0.000000000000000000, -15.23000000000000220, 27.00000000000000000 ) ) ;
#4939=CONICAL_SURFACE ( 'NONE', #2181, 2.024999999999999911, 0.7853981633974743692 ) ;
#4946=CARTESIAN_POINT ( 'NONE',  ( 1.999999999999994449, -45.00000000000000000, 23.99999999999999645 ) ) ;
#4952=DIRECTION ( 'NONE',  ( -1.000000000000000000, 0.000000000000000000, 0.000000000000000000 ) ) ;
#4957=ORIENTED_EDGE ( 'NONE', *, *, #13088, .F. ) ;
#4964=DIRECTION ( 'NONE',  ( 0.000000000000000000, 0.000000000000000000, 1.000000000000000000 ) ) ;
#4969=DIRECTION ( 'NONE',  ( -0.000000000000000000, -0.000000000000000000, -1.000000000000000000 ) ) ;
#4971=CARTESIAN_POINT ( 'NONE',  ( 41.49999999999999289, 27.79189783386526358, 27.00000000000000000 ) ) ;
#4973=LINE ( 'NONE', #14212, #22980 ) ;
#4976=DIRECTION ( 'NONE',  ( 1.000000000000000000, 0.000000000000000000, 0.000000000000000000 ) ) ;
#5008=CARTESIAN_POINT ( 'NONE',  ( 41.99999999999999289, 5.618459588085056979E-15, 0.000000000000000000 ) ) ;
#5022=ADVANCED_FACE ( 'NONE', ( #6001 ), #14569, .F. ) ;
#5030=ORIENTED_EDGE ( 'NONE', *, *, #13782, .T. ) ;
#5031=CARTESIAN_POINT ( 'NONE',  ( -14.99999999999999822, -6.045577542124163753E-21, 9.499999999999994671 ) ) ;
#5044=FACE_OUTER_BOUND ( 'NONE', #7608, .T. ) ;
#5050=DIRECTION ( 'NONE',  ( 0.000000000000000000, 0.000000000000000000, -1.000000000000000000 ) ) ;
#5054=ORIENTED_EDGE ( 'NONE', *, *, #16845, .F. ) ;
#5061=ORIENTED_EDGE ( 'NONE', *, *, #14442, .F. ) ;
#5067=DIRECTION ( 'NONE',  ( -0.000000000000000000, -0.000000000000000000, -1.000000000000000000 ) ) ;
#5073=DIRECTION ( 'NONE',  ( -0.000000000000000000, -0.000000000000000000, -1.000000000000000000 ) ) ;
#5080=VERTEX_POINT ( 'NONE', #6727 ) ;
#5084=EDGE_CURVE ( 'NONE', #3894, #5686, #10383, .T. ) ;
#5085=B_SPLINE_CURVE_WITH_KNOTS ( 'NONE', 3,
 ( #12516, #19988, #22296, #5461, #10696, #5222, #14727, #16206, #22189, #12414, #1463, #1565, #10571, #12651, #5099, #20118, #1336, #16422, #20230, #3147, #18166, #3394, #8872, #16313, #10917, #9696, #16911, #6064, #20835, #11399, #11272, #4117, #13010, #22781, #9335, #5932 ),
 .UNSPECIFIED., .F., .F.,
 ( 4, 2, 2, 2, 2, 2, 2, 2, 2, 2, 2, 2, 2, 2, 2, 2, 2, 4 ),
 ( 8.673617379884035472E-19, 0.002901772246161930194, 0.003627215307702410033, 0.004352658369242889437, 0.005803544492323848246, 0.006528987553864327650, 0.007254430615404807922, 0.008705316738485763262, 0.01015620286156672034, 0.01160708898464767394, 0.01305797510772863101, 0.01450886123080958809, 0.01595974735389054516, 0.01741063347697149877, 0.01886151960005245237, 0.02031240572313340598, 0.02176329184621436305, 0.02321417796929531666 ),
 .UNSPECIFIED. ) ;
#5099=CARTESIAN_POINT ( 'NONE',  ( 17.38700629636781869, 8.908123924593985166, 3.336041480784317503 ) ) ;
#5133=CARTESIAN_POINT ( 'NONE',  ( -14.51962751333974033, -3.765689428759031010, 27.00000000000000000 ) ) ;
#5134=VECTOR ( 'NONE', #11719, 1000.000000000000000 ) ;
#5136=ORIENTED_EDGE ( 'NONE', *, *, #16561, .F. ) ;
#5149=DIRECTION ( 'NONE',  ( -1.000000000000000000, 0.000000000000000000, 0.000000000000000000 ) ) ;
#5170=CIRCLE ( 'NONE', #7131, 4.999999999999997335 ) ;
#5173=DIRECTION ( 'NONE',  ( -0.000000000000000000, -0.000000000000000000, -1.000000000000000000 ) ) ;
#5182=DIRECTION ( 'NONE',  ( 1.000000000000000000, 0.000000000000000000, 0.000000000000000000 ) ) ;
#5201=VERTEX_POINT ( 'NONE', #14987 ) ;
#5208=CIRCLE ( 'NONE', #21972, 5.100000000000000533 ) ;
#5222=CARTESIAN_POINT ( 'NONE',  ( 16.36153765883235423, 6.593687918952694460, 6.842832175870693590 ) ) ;
#5224=ADVANCED_FACE ( 'NONE', ( #9486 ), #22464, .F. ) ;
#5234=DIRECTION ( 'NONE',  ( -0.000000000000000000, -0.000000000000000000, -1.000000000000000000 ) ) ;
#5242=CARTESIAN_POINT ( 'NONE',  ( 41.99999999999999289, 6.904644888889564703E-15, 10.50249999999999950 ) ) ;
#5246=CARTESIAN_POINT ( 'NONE',  ( 0.000000000000000000, -15.03999999999999915, -25.00000000000000000 ) ) ;
#5249=ORIENTED_EDGE ( 'NONE', *, *, #13555, .F. ) ;
#5256=CARTESIAN_POINT ( 'NONE',  ( -41.99999999999999289, 0.000000000000000000, 0.000000000000000000 ) ) ;
#5258=AXIS2_PLACEMENT_3D ( 'NONE', #4257, #17535, #5757 ) ;
#5265=ORIENTED_EDGE ( 'NONE', *, *, #11902, .T. ) ;
#5274=VECTOR ( 'NONE', #3934, 1000.000000000000114 ) ;
#5278=EDGE_LOOP ( 'NONE', ( #20804, #4193, #10154, #841 ) ) ;
#5287=DIRECTION ( 'NONE',  ( 0.000000000000000000, 0.000000000000000000, 1.000000000000000000 ) ) ;
#5288=CARTESIAN_POINT ( 'NONE',  ( 14.94708199919714531, -1.300481340138138098, 9.416259293296516120 ) ) ;
#5293=CARTESIAN_POINT ( 'NONE',  ( 14.51962751333974389, -3.765689428759035895, -27.00000000000000000 ) ) ;
#5294=AXIS2_PLACEMENT_3D ( 'NONE', #18093, #23232, #17722 ) ;
#5301=VERTEX_POINT ( 'NONE', #1595 ) ;
#5306=VERTEX_POINT ( 'NONE', #129 ) ;
#5307=VERTEX_POINT ( 'NONE', #1718 ) ;
#5323=DIRECTION ( 'NONE',  ( 0.000000000000000000, -1.000000000000000000, 0.000000000000000000 ) ) ;
#5324=EDGE_LOOP ( 'NONE', ( #18369, #994, #8295, #17309 ) ) ;
#5326=ORIENTED_EDGE ( 'NONE', *, *, #7673, .F. ) ;
#5329=VECTOR ( 'NONE', #17881, 1000.000000000000000 ) ;
#5337=CARTESIAN_POINT ( 'NONE',  ( -28.27483331787890819, -41.23752903419608629, -27.00000000000000000 ) ) ;
#5340=CARTESIAN_POINT ( 'NONE',  ( 0.000000000000000000, 45.00000000000000000, -27.00000000000000000 ) ) ;
#5352=ORIENTED_EDGE ( 'NONE', *, *, #19495, .F. ) ;
#5353=ORIENTED_EDGE ( 'NONE', *, *, #2100, .T. ) ;
#5356=DIRECTION ( 'NONE',  ( 0.000000000000000000, 0.000000000000000000, 1.000000000000000000 ) ) ;
#5381=AXIS2_PLACEMENT_3D ( 'NONE', #19923, #6750, #6518 ) ;
#5382=EDGE_LOOP ( 'NONE', ( #3805, #1920, #18954, #8393 ) ) ;
#5385=CARTESIAN_POINT ( 'NONE',  ( 1.999999999999994449, 45.00000000000000000, 26.97499999999999432 ) ) ;
#5392=FACE_OUTER_BOUND ( 'NONE', #913, .T. ) ;
#5405=CARTESIAN_POINT ( 'NONE',  ( 29.00000000000000711, -29.50000000000000711, -27.00000000000000000 ) ) ;
#5409=CARTESIAN_POINT ( 'NONE',  ( -23.84999999999999432, -15.03999999999999915, -25.00000000000000000 ) ) ;
#5412=ORIENTED_EDGE ( 'NONE', *, *, #4262, .F. ) ;
#5416=VERTEX_POINT ( 'NONE', #3836 ) ;
#5419=DIRECTION ( 'NONE',  ( 4.613626265895764052E-16, -1.000000000000000000, 0.000000000000000000 ) ) ;
#5420=CARTESIAN_POINT ( 'NONE',  ( 0.000000000000000000, 45.00000000000000000, 27.00000000000000000 ) ) ;
#5422=VERTEX_POINT ( 'NONE', #13469 ) ;
#5429=CARTESIAN_POINT ( 'NONE',  ( -39.99999999999999289, -29.50000000000001066, 27.00000000000000000 ) ) ;
#5448=EDGE_LOOP ( 'NONE', ( #5793, #14925, #7705, #68 ) ) ;
#5452=DIRECTION ( 'NONE',  ( 1.000000000000000000, 0.000000000000000000, 0.000000000000000000 ) ) ;
#5456=ORIENTED_EDGE ( 'NONE', *, *, #13561, .F. ) ;
#5461=CARTESIAN_POINT ( 'NONE',  ( 16.08510323282435195, 6.088885580147183063, 7.295537496892087859 ) ) ;
#5477=LINE ( 'NONE', #20355, #10259 ) ;
#5479=CARTESIAN_POINT ( 'NONE',  ( 2.024999999999999911, 45.00000000000000000, 27.00000000000000000 ) ) ;
#5482=( NAMED_UNIT ( * ) SI_UNIT ( $, .STERADIAN. ) SOLID_ANGLE_UNIT ( ) );
#5508=EDGE_LOOP ( 'NONE', ( #20554, #16548, #12842, #22397 ) ) ;
#5512=AXIS2_PLACEMENT_3D ( 'NONE', #7235, #14675, #4952 ) ;
#5524=ORIENTED_EDGE ( 'NONE', *, *, #3647, .F. ) ;
#5527=ORIENTED_EDGE ( 'NONE', *, *, #7793, .T. ) ;
#5533=AXIS2_PLACEMENT_3D ( 'NONE', #8073, #15519, #4689 ) ;
#5544=CARTESIAN_POINT ( 'NONE',  ( -14.94777716362147935, 1.291632522116891391, -9.417361603030281358 ) ) ;
#5567=DIRECTION ( 'NONE',  ( 1.000000000000000000, 0.000000000000000000, 0.000000000000000000 ) ) ;
#5585=EDGE_LOOP ( 'NONE', ( #12365, #16918, #23028, #19820, #10427, #22514, #616, #1343, #14933 ) ) ;
#5598=CIRCLE ( 'NONE', #19240, 20.85000000000000853 ) ;
#5611=CARTESIAN_POINT ( 'NONE',  ( -17.59008829125738060, 9.499485695642613692, -0.4958780962348213750 ) ) ;
#5616=VERTEX_POINT ( 'NONE', #19084 ) ;
#5620=CARTESIAN_POINT ( 'NONE',  ( -41.49999999999999289, -27.79189783386527779, -27.00000000000000000 ) ) ;
#5640=CARTESIAN_POINT ( 'NONE',  ( 0.000000000000000000, 15.03999999999999915, -27.00000000000000000 ) ) ;
#5641=AXIS2_PLACEMENT_3D ( 'NONE', #11209, #18681, #4630 ) ;
#5646=VECTOR ( 'NONE', #3378, 1000.000000000000000 ) ;
#5658=VECTOR ( 'NONE', #2415, 1000.000000000000000 ) ;
#5663=CARTESIAN_POINT ( 'NONE',  ( 34.10000000000001563, -29.50000000000000711, 27.00000000000000000 ) ) ;
#5666=CARTESIAN_POINT ( 'NONE',  ( -41.99999999999999289, 1.286185300804507526E-15, -10.50249999999999950 ) ) ;
#5672=CARTESIAN_POINT ( 'NONE',  ( 41.50000000000000000, -27.79189783386526358, -27.00000000000000000 ) ) ;
#5680=DIRECTION ( 'NONE',  ( -0.000000000000000000, -0.000000000000000000, -1.000000000000000000 ) ) ;
#5686=VERTEX_POINT ( 'NONE', #4946 ) ;
#5694=AXIS2_PLACEMENT_3D ( 'NONE', #4929, #12570, #16251 ) ;
#5700=CARTESIAN_POINT ( 'NONE',  ( 1.999999999999994449, -45.00000000000000000, -23.99999999999999645 ) ) ;
#5713=FACE_OUTER_BOUND ( 'NONE', #353, .T. ) ;
#5723=EDGE_CURVE ( 'NONE', #2790, #11994, #4836, .T. ) ;
#5728=CARTESIAN_POINT ( 'NONE',  ( -28.27483331787890819, -41.23752903419608629, 27.00000000000000000 ) ) ;
#5732=CARTESIAN_POINT ( 'NONE',  ( 23.84999999999999432, -15.03999999999999559, -25.00000000000000000 ) ) ;
#5735=CARTESIAN_POINT ( 'NONE',  ( -17.15849686392983031, 8.309918483244986831, 4.628645577532792821 ) ) ;
#5757=DIRECTION ( 'NONE',  ( -1.000000000000000000, 0.000000000000000000, 0.000000000000000000 ) ) ;
#5761=CARTESIAN_POINT ( 'NONE',  ( 0.000000000000000000, -45.00000000000000000, -27.00000000000000000 ) ) ;
#5762=CARTESIAN_POINT ( 'NONE',  ( 14.94708199919714531, 1.300481340138145203, -9.416259293296516120 ) ) ;
#5765=CARTESIAN_POINT ( 'NONE',  ( 29.00000000000000355, 29.50000000000000000, 27.00000000000000000 ) ) ;
#5772=CYLINDRICAL_SURFACE ( 'NONE', #23489, 18.50000000000000000 ) ;
#5779=DIRECTION ( 'NONE',  ( -0.000000000000000000, -0.000000000000000000, -1.000000000000000000 ) ) ;
#5790=VERTEX_POINT ( 'NONE', #19927 ) ;
#5793=ORIENTED_EDGE ( 'NONE', *, *, #7503, .T. ) ;
#5807=CARTESIAN_POINT ( 'NONE',  ( -41.49999999999999289, 27.79189783386526358, 27.00000000000000000 ) ) ;
#5822=ADVANCED_FACE ( 'NONE', ( #12945 ), #20285, .F. ) ;
#5825=CIRCLE ( 'NONE', #19474, 1.999999999999994449 ) ;
#5827=VERTEX_POINT ( 'NONE', #24061 ) ;
#5829=DIRECTION ( 'NONE',  ( 0.000000000000000000, 0.000000000000000000, 1.000000000000000000 ) ) ;
#5830=DIRECTION ( 'NONE',  ( -1.000000000000000000, 0.000000000000000000, 0.000000000000000000 ) ) ;
#5831=VECTOR ( 'NONE', #19493, 1000.000000000000000 ) ;
#5832=CIRCLE ( 'NONE', #22587, 18.49999999999999645 ) ;
#5850=CARTESIAN_POINT ( 'NONE',  ( 0.000000000000000000, -15.03999999999999915, -25.00000000000000000 ) ) ;
#5861=CONICAL_SURFACE ( 'NONE', #2344, 2.024999999999999911, 0.7853981633974743692 ) ;
#5866=FACE_BOUND ( 'NONE', #11406, .T. ) ;
#5882=CIRCLE ( 'NONE', #8217, 11.00000000000000000 ) ;
#5885=FACE_OUTER_BOUND ( 'NONE', #11555, .T. ) ;
#5889=CARTESIAN_POINT ( 'NONE',  ( -41.99999999999999289, 0.000000000000000000, 0.000000000000000000 ) ) ;
#5891=ORIENTED_EDGE ( 'NONE', *, *, #19464, .T. ) ;
#5892=AXIS2_PLACEMENT_3D ( 'NONE', #996, #10108, #1118 ) ;
#5895=ORIENTED_EDGE ( 'NONE', *, *, #23362, .T. ) ;
#5914=CARTESIAN_POINT ( 'NONE',  ( 29.00000000000000355, 29.50000000000000000, -27.00000000000000000 ) ) ;
#5922=CYLINDRICAL_SURFACE ( 'NONE', #2840, 9.499999999999987566 ) ;
#5926=EDGE_CURVE ( 'NONE', #12319, #14989, #13298, .T. ) ;
#5932=CARTESIAN_POINT ( 'NONE',  ( 14.51962751333974389, 3.765689428759031010, -8.721787840009197268 ) ) ;
#5935=VECTOR ( 'NONE', #15465, 1000.000000000000000 ) ;
#5952=CYLINDRICAL_SURFACE ( 'NONE', #8277, 1.500000000000001332 ) ;
#5959=CIRCLE ( 'NONE', #3221, 9.499999999999994671 ) ;
#5968=LINE ( 'NONE', #13400, #23097 ) ;
#5978=CARTESIAN_POINT ( 'NONE',  ( 0.000000000000000000, 0.000000000000000000, 0.000000000000000000 ) ) ;
#5988=LINE ( 'NONE', #11579, #17212 ) ;
#5989=STYLED_ITEM('',(#24134),#10155);
#5998=AXIS2_PLACEMENT_3D ( 'NONE', #17048, #15327, #18894 ) ;
#6001=FACE_OUTER_BOUND ( 'NONE', #3203, .T. ) ;
#6007=DIRECTION ( 'NONE',  ( -0.000000000000000000, -0.000000000000000000, -1.000000000000000000 ) ) ;
#6026=VECTOR ( 'NONE', #624, 1000.000000000000000 ) ;
#6032=DIRECTION ( 'NONE',  ( -0.000000000000000000, -0.000000000000000000, -1.000000000000000000 ) ) ;
#6035=ORIENTED_EDGE ( 'NONE', *, *, #21104, .T. ) ;
#6045=ORIENTED_EDGE ( 'NONE', *, *, #755, .F. ) ;
#6048=CARTESIAN_POINT ( 'NONE',  ( 1.999999999999994449, -45.00000000000000000, 27.00000000000000000 ) ) ;
#6052=VERTEX_POINT ( 'NONE', #5429 ) ;
#6060=AXIS2_PLACEMENT_3D ( 'NONE', #20740, #22573, #22471 ) ;
#6063=VECTOR ( 'NONE', #19407, 1000.000000000000000 ) ;
#6064=CARTESIAN_POINT ( 'NONE',  ( 16.82499651802897489, 7.532250541895348483, -5.808290850931483007 ) ) ;
#6070=ORIENTED_EDGE ( 'NONE', *, *, #21625, .T. ) ;
#6072=AXIS2_PLACEMENT_3D ( 'NONE', #348, #2043, #3883 ) ;
#6077=EDGE_CURVE ( 'NONE', #11604, #14761, #22988, .T. ) ;
#6091=CARTESIAN_POINT ( 'NONE',  ( -16.81886298599062002, 7.518780870797757920, -5.825851398835387940 ) ) ;
#6105=CARTESIAN_POINT ( 'NONE',  ( -20.85000000000000853, 15.04000000000000092, 27.00000000000000000 ) ) ;
#6113=ORIENTED_EDGE ( 'NONE', *, *, #3814, .F. ) ;
#6117=DIRECTION ( 'NONE',  ( -1.000000000000000000, 0.000000000000000000, 0.000000000000000000 ) ) ;
#6118=DIRECTION ( 'NONE',  ( -1.000000000000000000, 0.000000000000000000, 0.000000000000000000 ) ) ;
#6127=EDGE_CURVE ( 'NONE', #13972, #11452, #17617, .T. ) ;
#6144=ORIENTED_EDGE ( 'NONE', *, *, #15201, .F. ) ;
#6151=ADVANCED_FACE ( 'NONE', ( #19449 ), #15268, .F. ) ;
#6157=ORIENTED_EDGE ( 'NONE', *, *, #22390, .F. ) ;
#6171=AXIS2_PLACEMENT_3D ( 'NONE', #7740, #15435, #20458 ) ;
#6181=CARTESIAN_POINT ( 'NONE',  ( -34.10000000000000142, -29.50000000000001066, 27.00000000000000000 ) ) ;
#6189=EDGE_LOOP ( 'NONE', ( #19328, #30, #10030, #11850, #19103, #8656 ) ) ;
#6194=DIRECTION ( 'NONE',  ( 1.000000000000000000, 0.000000000000000000, 0.000000000000000000 ) ) ;
#6208=CARTESIAN_POINT ( 'NONE',  ( -15.78970982176773674, 5.581464347350853394, 7.700125654604360825 ) ) ;
#6211=EDGE_LOOP ( 'NONE', ( #6614, #18512, #3938, #4474 ) ) ;
#6215=CARTESIAN_POINT ( 'NONE',  ( -1.999999999999994449, 45.00000000000000000, 23.99999999999999645 ) ) ;
#6218=CARTESIAN_POINT ( 'NONE',  ( 40.89823313241238623, -26.41789760203348081, 27.00000000000000000 ) ) ;
#6229=CARTESIAN_POINT ( 'NONE',  ( -41.49999999999999289, 27.79189783386526358, -27.00000000000000000 ) ) ;
#6251=EDGE_CURVE ( 'NONE', #19379, #16743, #6387, .T. ) ;
#6265=ORIENTED_EDGE ( 'NONE', *, *, #7379, .F. ) ;
#6272=VERTEX_POINT ( 'NONE', #17864 ) ;
#6282=EDGE_CURVE ( 'NONE', #13474, #12890, #12600, .T. ) ;
#6288=DIRECTION ( 'NONE',  ( -0.000000000000000000, -0.000000000000000000, -1.000000000000000000 ) ) ;
#6292=CARTESIAN_POINT ( 'NONE',  ( 0.000000000000000000, 15.23000000000000220, -27.00000000000000000 ) ) ;
#6301=ORIENTED_EDGE ( 'NONE', *, *, #4905, .F. ) ;
#6307=DIRECTION ( 'NONE',  ( 1.000000000000000000, 0.000000000000000000, 0.000000000000000000 ) ) ;
#6309=ADVANCED_FACE ( 'NONE', ( #10633 ), #21647, .F. ) ;
#6316=AXIS2_PLACEMENT_3D ( 'NONE', #18436, #1726, #16598 ) ;
#6325=CIRCLE ( 'NONE', #9817, 4.999999999999997335 ) ;
#6326=CARTESIAN_POINT ( 'NONE',  ( 0.000000000000000000, -15.03999999999999915, -25.00000000000000000 ) ) ;
#6358=LINE ( 'NONE', #6850, #18327 ) ;
#6365=EDGE_LOOP ( 'NONE', ( #8547, #10066, #19782, #106 ) ) ;
#6368=CARTESIAN_POINT ( 'NONE',  ( -31.10231664966676135, -45.36128193761570770, 27.00000000000000000 ) ) ;
#6387=CIRCLE ( 'NONE', #23150, 11.00000000000000711 ) ;
#6391=DIRECTION ( 'NONE',  ( -0.000000000000000000, -0.000000000000000000, -1.000000000000000000 ) ) ;
#6394=DIRECTION ( 'NONE',  ( 1.000000000000000000, -0.000000000000000000, -0.000000000000000000 ) ) ;
#6400=DIRECTION ( 'NONE',  ( -0.000000000000000000, -0.000000000000000000, -1.000000000000000000 ) ) ;
#6405=ORIENTED_EDGE ( 'NONE', *, *, #251, .F. ) ;
#6406=ADVANCED_FACE ( 'NONE', ( #1860 ), #11101, .F. ) ;
#6416=CARTESIAN_POINT ( 'NONE',  ( -14.51962751333974033, -3.765689428759031010, -8.721787840009202597 ) ) ;
#6419=CARTESIAN_POINT ( 'NONE',  ( -17.52854577772372835, -9.313395544511447355, 1.935253206038904716 ) ) ;
#6420=DIRECTION ( 'NONE',  ( 1.000000000000000000, 0.000000000000000000, 0.000000000000000000 ) ) ;
#6424=CARTESIAN_POINT ( 'NONE',  ( -20.85000000000000853, 15.04000000000000092, -25.00000000000000000 ) ) ;
#6430=DIRECTION ( 'NONE',  ( -0.000000000000000000, -0.000000000000000000, 1.000000000000000000 ) ) ;
#6434=CARTESIAN_POINT ( 'NONE',  ( 14.91624121966758842, 1.615102390220948037, 9.367332145225617523 ) ) ;
#6446=ORIENTED_EDGE ( 'NONE', *, *, #16933, .T. ) ;
#6453=FACE_OUTER_BOUND ( 'NONE', #14229, .T. ) ;
#6461=DIRECTION ( 'NONE',  ( -0.000000000000000000, -0.000000000000000000, 1.000000000000000000 ) ) ;
#6462=ORIENTED_EDGE ( 'NONE', *, *, #10988, .T. ) ;
#6474=CARTESIAN_POINT ( 'NONE',  ( 18.50000000000000000, 15.23000000000000398, 27.00000000000000000 ) ) ;
#6502=EDGE_CURVE ( 'NONE', #7988, #4702, #5959, .T. ) ;
#6515=VECTOR ( 'NONE', #21747, 1000.000000000000000 ) ;
#6517=ORIENTED_EDGE ( 'NONE', *, *, #13555, .T. ) ;
#6518=DIRECTION ( 'NONE',  ( -1.000000000000000000, 0.000000000000000000, 0.000000000000000000 ) ) ;
#6524=LINE ( 'NONE', #12094, #16879 ) ;
#6527=APPLICATION_CONTEXT ( 'automotive_design' ) ;
#6530=EDGE_CURVE ( 'NONE', #3165, #8486, #11699, .T. ) ;
#6532=VERTEX_POINT ( 'NONE', #4420 ) ;
#6544=CARTESIAN_POINT ( 'NONE',  ( -16.36153765883235423, -6.593687918952691795, 6.842832175870698919 ) ) ;
#6551=DIRECTION ( 'NONE',  ( -1.000000000000000000, 0.000000000000000000, 0.000000000000000000 ) ) ;
#6552=CARTESIAN_POINT ( 'NONE',  ( 30.44534269664590909, -40.40463133211080304, 27.00000000000000000 ) ) ;
#6555=AXIS2_PLACEMENT_3D ( 'NONE', #11611, #6391, #2238 ) ;
#6556=CARTESIAN_POINT ( 'NONE',  ( 14.98952570844869747, 0.6468970097546595799, 9.483487670324109331 ) ) ;
#6564=ORIENTED_EDGE ( 'NONE', *, *, #1411, .T. ) ;
#6570=CIRCLE ( 'NONE', #9648, 5.100000000000000533 ) ;
#6579=CARTESIAN_POINT ( 'NONE',  ( -28.99999999999999645, 29.50000000000000000, 27.00000000000000000 ) ) ;
#6586=CYLINDRICAL_SURFACE ( 'NONE', #13809, 20.85000000000000142 ) ;
#6603=EDGE_CURVE ( 'NONE', #22613, #8771, #11769, .T. ) ;
#6607=DIRECTION ( 'NONE',  ( 1.000000000000000000, 0.000000000000000000, 0.000000000000000000 ) ) ;
#6609=DIRECTION ( 'NONE',  ( -0.8571673007021116675, 1.049727191138617833E-16, 0.5150380749100552658 ) ) ;
#6614=ORIENTED_EDGE ( 'NONE', *, *, #3572, .T. ) ;
#6616=LINE ( 'NONE', #19907, #22693 ) ;
#6618=B_SPLINE_CURVE_WITH_KNOTS ( 'NONE', 3,
 ( #6668, #3016, #18005, #19483, #17895, #1183, #23639, #13874, #2884, #19848, #3119, #4610, #8596, #6912, #16043, #10542, #23505, #10175, #15816, #11899, #8723, #6786, #14216, #16175, #14332, #17632, #23148, #4490, #19372, #12012, #3362, #1888, #3239, #20202, #3588, #1433 ),
 .UNSPECIFIED., .F., .F.,
 ( 4, 2, 2, 2, 2, 2, 2, 2, 2, 2, 2, 2, 2, 2, 2, 2, 2, 4 ),
 ( 3.004629197474318463E-18, 0.002901772246161926725, 0.003627215307702404828, 0.004352658369242881631, 0.005803544492323830899, 0.006528987553864306834, 0.007254430615404782769, 0.008705316738485735506, 0.01015620286156668911, 0.01160708898464764098, 0.01305797510772859632, 0.01450886123080954992, 0.01595974735389050353, 0.01741063347697145713, 0.01886151960005241074, 0.02031240572313336781, 0.02176329184621432142, 0.02321417796929527502 ),
 .UNSPECIFIED. ) ;
#6624=ORIENTED_EDGE ( 'NONE', *, *, #19495, .T. ) ;
#6632=DIRECTION ( 'NONE',  ( 1.000000000000000000, 0.000000000000000000, 0.000000000000000000 ) ) ;
#6633=VERTEX_POINT ( 'NONE', #22963 ) ;
#6649=ORIENTED_EDGE ( 'NONE', *, *, #3122, .T. ) ;
#6657=EDGE_CURVE ( 'NONE', #20027, #18466, #389, .T. ) ;
#6668=CARTESIAN_POINT ( 'NONE',  ( 14.51962751333974211, -3.765689428759034563, -8.721787840009190163 ) ) ;
#6690=ORIENTED_EDGE ( 'NONE', *, *, #15703, .T. ) ;
#6693=CARTESIAN_POINT ( 'NONE',  ( 0.000000000000000000, 15.23000000000000220, 27.00000000000000000 ) ) ;
#6711=VECTOR ( 'NONE', #9349, 1000.000000000000000 ) ;
#6718=CARTESIAN_POINT ( 'NONE',  ( -23.89999999999999858, 29.50000000000000000, 27.00000000000000000 ) ) ;
#6724=EDGE_LOOP ( 'NONE', ( #6794, #9643, #16529, #6462 ) ) ;
#6727=CARTESIAN_POINT ( 'NONE',  ( 42.00000000000000000, -25.93535998569253920, 27.00000000000000000 ) ) ;
#6732=AXIS2_PLACEMENT_3D ( 'NONE', #12412, #10343, #8517 ) ;
#6735=VECTOR ( 'NONE', #9881, 1000.000000000000000 ) ;
#6750=DIRECTION ( 'NONE',  ( 0.000000000000000000, 0.000000000000000000, 1.000000000000000000 ) ) ;
#6757=EDGE_LOOP ( 'NONE', ( #13745, #22610, #19654, #12735 ) ) ;
#6776=CARTESIAN_POINT ( 'NONE',  ( -17.06033556854818656, -8.068938288216807919, -5.036196554528634017 ) ) ;
#6778=ORIENTED_EDGE ( 'NONE', *, *, #19102, .F. ) ;
#6786=CARTESIAN_POINT ( 'NONE',  ( 17.52920230446416028, -9.315347328456290654, 1.925892650121551419 ) ) ;
#6794=ORIENTED_EDGE ( 'NONE', *, *, #13419, .T. ) ;
#6796=ORIENTED_EDGE ( 'NONE', *, *, #10988, .F. ) ;
#6802=CARTESIAN_POINT ( 'NONE',  ( 0.000000000000000000, 0.000000000000000000, 27.00000000000000000 ) ) ;
#6805=DIRECTION ( 'NONE',  ( -1.000000000000000000, 0.000000000000000000, 0.000000000000000000 ) ) ;
#6808=CONICAL_SURFACE ( 'NONE', #4462, 10.50249999999999950, 0.7853981633974491672 ) ;
#6814=CIRCLE ( 'NONE', #18120, 5.100000000000000533 ) ;
#6825=ORIENTED_EDGE ( 'NONE', *, *, #18150, .T. ) ;
#6830=EDGE_CURVE ( 'NONE', #4702, #20316, #11165, .T. ) ;
#6845=CYLINDRICAL_SURFACE ( 'NONE', #5892, 49.99999999999999289 ) ;
#6850=CARTESIAN_POINT ( 'NONE',  ( -1.999999999999994449, 45.00000000000000000, 23.99999999999999645 ) ) ;
#6852=AXIS2_PLACEMENT_3D ( 'NONE', #4481, #17141, #15172 ) ;
#6855=ORIENTED_EDGE ( 'NONE', *, *, #13570, .T. ) ;
#6861=DIRECTION ( 'NONE',  ( 1.000000000000000000, 0.000000000000000000, 0.000000000000000000 ) ) ;
#6874=VERTEX_POINT ( 'NONE', #20592 ) ;
#6885=VECTOR ( 'NONE', #15457, 1000.000000000000000 ) ;
#6889=EDGE_CURVE ( 'NONE', #14835, #13696, #3756, .T. ) ;
#6895=ORIENTED_EDGE ( 'NONE', *, *, #4493, .T. ) ;
#6901=CARTESIAN_POINT ( 'NONE',  ( -16.44572538483723534, -6.755397553796130161, 6.683320200552561374 ) ) ;
#6902=EDGE_CURVE ( 'NONE', #14244, #13664, #526, .T. ) ;
#6910=CARTESIAN_POINT ( 'NONE',  ( 0.000000000000000000, 0.000000000000000000, 27.00000000000000000 ) ) ;
#6912=CARTESIAN_POINT ( 'NONE',  ( 17.32141611691247718, -8.728455122802969868, -3.780491077225275998 ) ) ;
#6917=EDGE_LOOP ( 'NONE', ( #10351, #6113, #1839, #17343 ) ) ;
#6934=ADVANCED_FACE ( 'NONE', ( #4857 ), #18252, .T. ) ;
#6938=LINE ( 'NONE', #2917, #11766 ) ;
#6951=ORIENTED_EDGE ( 'NONE', *, *, #16151, .F. ) ;
#6963=CARTESIAN_POINT ( 'NONE',  ( -1.999999999999994449, 45.00000000000000000, -27.00000000000000000 ) ) ;
#6969=CARTESIAN_POINT ( 'NONE',  ( 28.27483331787887622, 41.23752903419610050, -27.00000000000000000 ) ) ;
#6982=CARTESIAN_POINT ( 'NONE',  ( 0.000000000000000000, 45.00000000000000000, -26.97499999999999432 ) ) ;
#7030=DIRECTION ( 'NONE',  ( -0.000000000000000000, -0.000000000000000000, -1.000000000000000000 ) ) ;
#7035=CARTESIAN_POINT ( 'NONE',  ( 20.85000000000000853, 15.03999999999999915, -27.00000000000000000 ) ) ;
#7041=ORIENTED_EDGE ( 'NONE', *, *, #13110, .F. ) ;
#7051=ORIENTED_EDGE ( 'NONE', *, *, #2179, .T. ) ;
#7060=AXIS2_PLACEMENT_3D ( 'NONE', #3521, #19885, #21831 ) ;
#7069=DIRECTION ( 'NONE',  ( 1.000000000000000000, 0.000000000000000000, 0.000000000000000000 ) ) ;
#7076=ORIENTED_EDGE ( 'NONE', *, *, #7674, .F. ) ;
#7077=CARTESIAN_POINT ( 'NONE',  ( -39.99999999999999289, 29.50000000000000000, -27.00000000000000000 ) ) ;
#7086=AXIS2_PLACEMENT_3D ( 'NONE', #20666, #414, #18837 ) ;
#7093=CARTESIAN_POINT ( 'NONE',  ( 40.00000000000000000, -29.50000000000000000, 27.00000000000000000 ) ) ;
#7094=VECTOR ( 'NONE', #8618, 1000.000000000000000 ) ;
#7095=VECTOR ( 'NONE', #18518, 1000.000000000000000 ) ;
#7102=EDGE_CURVE ( 'NONE', #16743, #24058, #20798, .T. ) ;
#7113=AXIS2_PLACEMENT_3D ( 'NONE', #19505, #13897, #2781 ) ;
#7119=VECTOR ( 'NONE', #756, 1000.000000000000000 ) ;
#7131=AXIS2_PLACEMENT_3D ( 'NONE', #4229, #6288, #18997 ) ;
#7162=CARTESIAN_POINT ( 'NONE',  ( -18.49999999999999645, -15.23000000000000220, -27.00000000000000000 ) ) ;
#7166=AXIS2_PLACEMENT_3D ( 'NONE', #8623, #6461, #4883 ) ;
#7167=CARTESIAN_POINT ( 'NONE',  ( -1.029124893018731811E-15, 45.00000000000000000, -22.79827876194487857 ) ) ;
#7199=CARTESIAN_POINT ( 'NONE',  ( -14.98950073861089294, 0.6491375924673337128, 9.483449329262338523 ) ) ;
#7205=FACE_BOUND ( 'NONE', #18325, .T. ) ;
#7208=DIRECTION ( 'NONE',  ( 1.000000000000000000, -0.000000000000000000, -0.000000000000000000 ) ) ;
#7209=ORIENTED_EDGE ( 'NONE', *, *, #22125, .F. ) ;
#7216=AXIS2_PLACEMENT_3D ( 'NONE', #17554, #1110, #12180 ) ;
#7222=CARTESIAN_POINT ( 'NONE',  ( 31.10231664966676846, -45.36128193761570770, 27.00000000000000000 ) ) ;
#7228=ADVANCED_FACE ( 'NONE', ( #2732 ), #15644, .F. ) ;
#7230=CARTESIAN_POINT ( 'NONE',  ( -18.50000000000000000, 15.23000000000000220, 27.00000000000000000 ) ) ;
#7235=CARTESIAN_POINT ( 'NONE',  ( 0.000000000000000000, 0.000000000000000000, 27.00000000000000000 ) ) ;
#7253=EDGE_CURVE ( 'NONE', #17283, #23345, #2473, .T. ) ;
#7271=ORIENTED_EDGE ( 'NONE', *, *, #2239, .F. ) ;
#7277=CARTESIAN_POINT ( 'NONE',  ( -34.10000000000000142, -29.50000000000001066, 27.00000000000000000 ) ) ;
#7278=CARTESIAN_POINT ( 'NONE',  ( 23.84999999999999432, -15.03999999999999559, -25.00000000000000000 ) ) ;
#7283=ADVANCED_FACE ( 'NONE', ( #7964 ), #19344, .F. ) ;
#7286=DIRECTION ( 'NONE',  ( -0.000000000000000000, -0.000000000000000000, -1.000000000000000000 ) ) ;
#7288=LINE ( 'NONE', #14728, #10691 ) ;
#7321=LINE ( 'NONE', #3663, #1309 ) ;
#7325=DIRECTION ( 'NONE',  ( -0.000000000000000000, 0.000000000000000000, -1.000000000000000000 ) ) ;
#7333=DIRECTION ( 'NONE',  ( -0.000000000000000000, -0.000000000000000000, -1.000000000000000000 ) ) ;
#7337=CIRCLE ( 'NONE', #20633, 5.100000000000000533 ) ;
#7340=ORIENTED_EDGE ( 'NONE', *, *, #17211, .T. ) ;
#7341=DIRECTION ( 'NONE',  ( -1.000000000000000000, 0.000000000000000000, 0.000000000000000000 ) ) ;
#7348=EDGE_LOOP ( 'NONE', ( #23467, #13145, #10441, #19141 ) ) ;
#7362=CARTESIAN_POINT ( 'NONE',  ( 40.89823313241238623, -26.41789760203348081, 27.00000000000000000 ) ) ;
#7379=EDGE_CURVE ( 'NONE', #19404, #8356, #23827, .T. ) ;
#7389=ORIENTED_EDGE ( 'NONE', *, *, #7674, .T. ) ;
#7393=DIRECTION ( 'NONE',  ( 1.000000000000000000, 0.000000000000000000, -0.000000000000000000 ) ) ;
#7411=CARTESIAN_POINT ( 'NONE',  ( -17.49066032632880763, 9.200828712690867661, -2.414248458042551171 ) ) ;
#7414=CARTESIAN_POINT ( 'NONE',  ( 14.51962751333974389, 3.765689428759031010, -8.721787840009197268 ) ) ;
#7415=ADVANCED_FACE ( 'NONE', ( #10520 ), #18110, .F. ) ;
#7420=EDGE_CURVE ( 'NONE', #24058, #22047, #12592, .T. ) ;
#7434=CARTESIAN_POINT ( 'NONE',  ( -14.51962751333974389, 3.765689428759031010, 27.00000000000000000 ) ) ;
#7442=ORIENTED_EDGE ( 'NONE', *, *, #21625, .F. ) ;
#7453=ORIENTED_EDGE ( 'NONE', *, *, #19171, .T. ) ;
#7454=CARTESIAN_POINT ( 'NONE',  ( -23.85000000000000497, 15.03999999999999915, 27.00000000000000000 ) ) ;
#7460=DIRECTION ( 'NONE',  ( -1.000000000000000000, 0.000000000000000000, 0.000000000000000000 ) ) ;
#7484=CARTESIAN_POINT ( 'NONE',  ( 14.51962751333974389, 3.765689428759029234, 27.00000000000000000 ) ) ;
#7491=CARTESIAN_POINT ( 'NONE',  ( 41.99999999999999289, 5.618459588085056979E-15, -9.499999999999987566 ) ) ;
#7500=CARTESIAN_POINT ( 'NONE',  ( 0.000000000000000000, 0.000000000000000000, 27.00000000000000000 ) ) ;
#7501=DIRECTION ( 'NONE',  ( -0.000000000000000000, -0.000000000000000000, 1.000000000000000000 ) ) ;
#7503=EDGE_CURVE ( 'NONE', #22892, #10927, #6325, .T. ) ;
#7516=AXIS2_PLACEMENT_3D ( 'NONE', #17946, #8650, #10599 ) ;
#7518=CIRCLE ( 'NONE', #14159, 5.100000000000000533 ) ;
#7524=CARTESIAN_POINT ( 'NONE',  ( -39.99999999999999289, 29.50000000000000000, 27.00000000000000000 ) ) ;
#7526=EDGE_CURVE ( 'NONE', #7845, #11886, #22137, .T. ) ;
#7528=CARTESIAN_POINT ( 'NONE',  ( 28.27483331787887622, 41.23752903419610050, 27.00000000000000000 ) ) ;
#7531=DIRECTION ( 'NONE',  ( 0.000000000000000000, -1.000000000000000000, 0.000000000000000000 ) ) ;
#7541=VERTEX_POINT ( 'NONE', #5409 ) ;
#7547=AXIS2_PLACEMENT_3D ( 'NONE', #23771, #9983, #18279 ) ;
#7549=CARTESIAN_POINT ( 'NONE',  ( -41.99999999999999289, 25.93535998569253920, 27.00000000000000000 ) ) ;
#7550=DIRECTION ( 'NONE',  ( 0.000000000000000000, 0.000000000000000000, 1.000000000000000000 ) ) ;
#7583=AXIS2_PLACEMENT_3D ( 'NONE', #12287, #21809, #20108 ) ;
#7585=ORIENTED_EDGE ( 'NONE', *, *, #11240, .F. ) ;
#7586=ORIENTED_EDGE ( 'NONE', *, *, #22246, .F. ) ;
#7594=DIRECTION ( 'NONE',  ( -0.000000000000000000, -0.000000000000000000, 1.000000000000000000 ) ) ;
#7608=EDGE_LOOP ( 'NONE', ( #5527, #15535, #8115, #9225 ) ) ;
#7615=CIRCLE ( 'NONE', #13889, 20.85000000000000853 ) ;
#7616=EDGE_LOOP ( 'NONE', ( #6157, #18290, #11018, #1719 ) ) ;
#7618=CARTESIAN_POINT ( 'NONE',  ( 14.51962751333974211, -3.765689428759034563, -8.721787840009190163 ) ) ;
#7619=CYLINDRICAL_SURFACE ( 'NONE', #19016, 1.500000000000001332 ) ;
#7620=ADVANCED_FACE ( 'NONE', ( #13302 ), #20768, .T. ) ;
#7628=CARTESIAN_POINT ( 'NONE',  ( -40.89823313241237912, 26.41789760203348081, 27.00000000000000000 ) ) ;
#7630=LINE ( 'NONE', #9230, #21954 ) ;
#7631=DIRECTION ( 'NONE',  ( 1.000000000000000000, 0.000000000000000000, 0.000000000000000000 ) ) ;
#7648=CARTESIAN_POINT ( 'NONE',  ( -14.51962751333974033, -3.765689428759031010, -27.00000000000000000 ) ) ;
#7651=CIRCLE ( 'NONE', #21322, 1.500000000000001332 ) ;
#7654=ORIENTED_EDGE ( 'NONE', *, *, #8377, .T. ) ;
#7656=DIRECTION ( 'NONE',  ( -0.000000000000000000, -0.000000000000000000, 1.000000000000000000 ) ) ;
#7658=CARTESIAN_POINT ( 'NONE',  ( -16.68617496892350260, 7.233372502334340481, 6.175747996014763430 ) ) ;
#7671=LINE ( 'NONE', #6105, #9160 ) ;
#7673=EDGE_CURVE ( 'NONE', #22991, #16629, #6616, .T. ) ;
#7674=EDGE_CURVE ( 'NONE', #16347, #8203, #4792, .T. ) ;
#7680=CIRCLE ( 'NONE', #11192, 2.024999999999999911 ) ;
#7696=VERTEX_POINT ( 'NONE', #8796 ) ;
#7697=AXIS2_PLACEMENT_3D ( 'NONE', #2381, #18739, #2147 ) ;
#7700=VERTEX_POINT ( 'NONE', #16241 ) ;
#7702=EDGE_CURVE ( 'NONE', #23460, #13664, #17844, .T. ) ;
#7703=EDGE_CURVE ( 'NONE', #5301, #678, #18791, .T. ) ;
#7705=ORIENTED_EDGE ( 'NONE', *, *, #2100, .F. ) ;
#7708=EDGE_LOOP ( 'NONE', ( #17079, #3434, #13253, #15622 ) ) ;
#7709=CYLINDRICAL_SURFACE ( 'NONE', #6555, 5.100000000000000533 ) ;
#7710=ORIENTED_EDGE ( 'NONE', *, *, #16151, .T. ) ;
#7722=EDGE_LOOP ( 'NONE', ( #22965, #15048, #20764, #17392 ) ) ;
#7726=CLOSED_SHELL ( 'NONE', ( #8183, #10565, #16969, #17991, #10446, #5022, #3831, #14949, #10910, #14966, #16007, #20444, #13884, #22626, #1442, #1212, #8120, #1837, #3143, #9060, #23522, #715, #3115, #1580, #19648, #22698, #5822, #8702, #2163, #15084, #24013, #10072, #3323, #9680, #15557, #12002, #22834, #1875, #3411, #16758, #18631, #19899, #18375, #2005, #11973, #14247, #9371, #6309, #7937, #14915, #22036, #15182, #18726, #12168, #7620, #8696, #7283, #7415, #6406, #1475, #6151, #16034, #17204, #7228, #22944, #23247, #23835, #3674, #2462, #23226, #3808, #19298, #18188, #17242, #8499, #21649, #5224, #8997, #6934, #14546, #20439, #10235, #11190, #4706, #1410, #12960, #21496, #9274, #20412, #14682, #905, #23574, #21644, #16496, #14169, #22300, #19612, #10626 ) ) ;
#7733=EDGE_CURVE ( 'NONE', #5307, #4702, #20376, .T. ) ;
#7740=CARTESIAN_POINT ( 'NONE',  ( -23.85000000000000497, 15.03999999999999915, 25.00000000000000000 ) ) ;
#7742=DIRECTION ( 'NONE',  ( 1.000000000000000000, 0.000000000000000000, -0.000000000000000000 ) ) ;
#7753=EDGE_LOOP ( 'NONE', ( #6895, #3265, #17166, #13135, #17448, #2724 ) ) ;
#7756=ORIENTED_EDGE ( 'NONE', *, *, #11463, .T. ) ;
#7765=CARTESIAN_POINT ( 'NONE',  ( 40.00000000000000000, -29.50000000000000000, 27.00000000000000000 ) ) ;
#7766=DIRECTION ( 'NONE',  ( 1.000000000000000000, 0.000000000000000000, 0.000000000000000000 ) ) ;
#7769=CARTESIAN_POINT ( 'NONE',  ( -17.05196227081077964, 8.053793831531468328, -5.044162359773903148 ) ) ;
#7777=EDGE_CURVE ( 'NONE', #2350, #20120, #7321, .T. ) ;
#7780=( LENGTH_UNIT ( ) NAMED_UNIT ( * ) SI_UNIT ( .MILLI., .METRE. ) );
#7783=CARTESIAN_POINT ( 'NONE',  ( -41.99999999999999289, -25.93535998569255341, 27.00000000000000000 ) ) ;
#7793=EDGE_CURVE ( 'NONE', #7700, #21154, #9837, .T. ) ;
#7795=CARTESIAN_POINT ( 'NONE',  ( -23.89999999999999858, -29.50000000000001066, 27.00000000000000000 ) ) ;
#7804=EDGE_CURVE ( 'NONE', #22047, #18868, #23103, .T. ) ;
#7809=ORIENTED_EDGE ( 'NONE', *, *, #19855, .T. ) ;
#7815=LINE ( 'NONE', #4199, #22885 ) ;
#7821=CARTESIAN_POINT ( 'NONE',  ( -31.10231664966676135, 45.36128193761570770, -27.00000000000000000 ) ) ;
#7823=CIRCLE ( 'NONE', #11331, 4.999999999999997335 ) ;
#7845=VERTEX_POINT ( 'NONE', #5385 ) ;
#7848=CARTESIAN_POINT ( 'NONE',  ( -18.49999999999999645, -15.23000000000000220, 27.00000000000000000 ) ) ;
#7861=VECTOR ( 'NONE', #16576, 1000.000000000000000 ) ;
#7877=DIRECTION ( 'NONE',  ( -1.000000000000000000, 0.000000000000000000, 0.000000000000000000 ) ) ;
#7891=CARTESIAN_POINT ( 'NONE',  ( -14.51962751333974211, 3.765689428759028790, -8.721787840009202597 ) ) ;
#7920=CIRCLE ( 'NONE', #21600, 11.00000000000000355 ) ;
#7922=FACE_OUTER_BOUND ( 'NONE', #13847, .T. ) ;
#7931=VERTEX_POINT ( 'NONE', #1296 ) ;
#7935=CARTESIAN_POINT ( 'NONE',  ( 23.85000000000000497, 15.03999999999999915, 27.00000000000000000 ) ) ;
#7937=ADVANCED_FACE ( 'NONE', ( #12489 ), #12260, .F. ) ;
#7946=ORIENTED_EDGE ( 'NONE', *, *, #7702, .F. ) ;
#7955=DIRECTION ( 'NONE',  ( -1.000000000000000000, 0.000000000000000000, 0.000000000000000000 ) ) ;
#7964=FACE_OUTER_BOUND ( 'NONE', #1745, .T. ) ;
#7988=VERTEX_POINT ( 'NONE', #20752 ) ;
#8002=ORIENTED_EDGE ( 'NONE', *, *, #12106, .F. ) ;
#8004=VERTEX_POINT ( 'NONE', #18799 ) ;
#8005=AXIS2_PLACEMENT_3D ( 'NONE', #5978, #22344, #13412 ) ;
#8049=DIRECTION ( 'NONE',  ( -1.000000000000000000, 0.000000000000000000, 0.000000000000000000 ) ) ;
#8052=ORIENTED_EDGE ( 'NONE', *, *, #14977, .F. ) ;
#8063=VERTEX_POINT ( 'NONE', #15007 ) ;
#8073=CARTESIAN_POINT ( 'NONE',  ( 0.000000000000000000, 0.000000000000000000, 27.00000000000000000 ) ) ;
#8076=EDGE_CURVE ( 'NONE', #588, #16629, #1304, .T. ) ;
#8080=CARTESIAN_POINT ( 'NONE',  ( 0.000000000000000000, 0.000000000000000000, 27.00000000000000000 ) ) ;
#8083=CIRCLE ( 'NONE', #14330, 4.999999999999997335 ) ;
#8086=ORIENTED_EDGE ( 'NONE', *, *, #4575, .F. ) ;
#8107=CARTESIAN_POINT ( 'NONE',  ( -1.999999999999994449, -45.00000000000000000, -23.99999999999999645 ) ) ;
#8109=FACE_BOUND ( 'NONE', #7348, .T. ) ;
#8115=ORIENTED_EDGE ( 'NONE', *, *, #7703, .F. ) ;
#8120=ADVANCED_FACE ( 'NONE', ( #15743 ), #4781, .F. ) ;
#8121=ORIENTED_EDGE ( 'NONE', *, *, #15877, .F. ) ;
#8122=VECTOR ( 'NONE', #2698, 1000.000000000000000 ) ;
#8134=CYLINDRICAL_SURFACE ( 'NONE', #2825, 1.999999999999994449 ) ;
#8144=EDGE_CURVE ( 'NONE', #6052, #18241, #17563, .T. ) ;
#8148=AXIS2_PLACEMENT_3D ( 'NONE', #6910, #23635, #10431 ) ;
#8152=LINE ( 'NONE', #15596, #14207 ) ;
#8156=DIRECTION ( 'NONE',  ( -0.000000000000000000, -0.000000000000000000, -1.000000000000000000 ) ) ;
#8163=EDGE_CURVE ( 'NONE', #23091, #23565, #10991, .T. ) ;
#8164=ORIENTED_EDGE ( 'NONE', *, *, #7526, .T. ) ;
#8165=CARTESIAN_POINT ( 'NONE',  ( 40.00000000000000000, -29.50000000000000000, -27.00000000000000000 ) ) ;
#8166=CARTESIAN_POINT ( 'NONE',  ( 1.999999999999994449, -45.00000000000000000, 26.97499999999999432 ) ) ;
#8183=ADVANCED_FACE ( 'NONE', ( #23206 ), #16090, .F. ) ;
#8194=ORIENTED_EDGE ( 'NONE', *, *, #11240, .T. ) ;
#8199=CARTESIAN_POINT ( 'NONE',  ( 14.51962751333974211, -3.765689428759034563, 8.721787840009190163 ) ) ;
#8203=VERTEX_POINT ( 'NONE', #8786 ) ;
#8204=ORIENTED_EDGE ( 'NONE', *, *, #21227, .T. ) ;
#8210=AXIS2_PLACEMENT_3D ( 'NONE', #21486, #13795, #17945 ) ;
#8217=AXIS2_PLACEMENT_3D ( 'NONE', #14952, #22187, #3504 ) ;
#8223=DIRECTION ( 'NONE',  ( -0.000000000000000000, -0.000000000000000000, 1.000000000000000000 ) ) ;
#8224=LINE ( 'NONE', #14213, #13699 ) ;
#8225=CARTESIAN_POINT ( 'NONE',  ( -15.00000000000000178, -0.3238088414458164532, 9.499999999999998224 ) ) ;
#8259=DIRECTION ( 'NONE',  ( 1.000000000000000000, 0.000000000000000000, 0.000000000000000000 ) ) ;
#8261=AXIS2_PLACEMENT_3D ( 'NONE', #23804, #12556, #3313 ) ;
#8262=DIRECTION ( 'NONE',  ( -0.000000000000000000, -0.000000000000000000, -1.000000000000000000 ) ) ;
#8277=AXIS2_PLACEMENT_3D ( 'NONE', #350, #15091, #20857 ) ;
#8283=LINE ( 'NONE', #21240, #17208 ) ;
#8287=EDGE_CURVE ( 'NONE', #8820, #24058, #15280, .T. ) ;
#8295=ORIENTED_EDGE ( 'NONE', *, *, #18228, .F. ) ;
#8304=CARTESIAN_POINT ( 'NONE',  ( -20.85000000000000142, -15.03999999999999915, -27.00000000000000000 ) ) ;
#8307=CARTESIAN_POINT ( 'NONE',  ( 40.89823313241238623, -26.41789760203348081, -27.00000000000000000 ) ) ;
#8334=CARTESIAN_POINT ( 'NONE',  ( 29.00000000000000711, -29.50000000000000711, 27.00000000000000000 ) ) ;
#8343=CONICAL_SURFACE ( 'NONE', #4070, 2.024999999999999911, 0.7853981633974743692 ) ;
#8352=CARTESIAN_POINT ( 'NONE',  ( -15.56475192642547967, -5.220978644676160130, -7.947934502462941531 ) ) ;
#8353=DIRECTION ( 'NONE',  ( -0.000000000000000000, -0.000000000000000000, 1.000000000000000000 ) ) ;
#8354=EDGE_CURVE ( 'NONE', #128, #11857, #5968, .T. ) ;
#8356=VERTEX_POINT ( 'NONE', #20863 ) ;
#8377=EDGE_CURVE ( 'NONE', #16629, #588, #12558, .T. ) ;
#8380=UNCERTAINTY_MEASURE_WITH_UNIT (LENGTH_MEASURE( 1.000000000000000082E-05 ), #7780, 'distance_accuracy_value', 'NONE');
#8384=CYLINDRICAL_SURFACE ( 'NONE', #11517, 20.85000000000000853 ) ;
#8385=DIRECTION ( 'NONE',  ( -0.000000000000000000, -0.000000000000000000, -1.000000000000000000 ) ) ;
#8393=ORIENTED_EDGE ( 'NONE', *, *, #2463, .T. ) ;
#8407=ORIENTED_EDGE ( 'NONE', *, *, #6902, .T. ) ;
#8424=CARTESIAN_POINT ( 'NONE',  ( 0.000000000000000000, 45.00000000000000000, -27.00000000000000000 ) ) ;
#8428=DIRECTION ( 'NONE',  ( -1.000000000000000000, 0.000000000000000000, 0.000000000000000000 ) ) ;
#8432=EDGE_CURVE ( 'NONE', #5616, #7931, #17377, .T. ) ;
#8438=ORIENTED_EDGE ( 'NONE', *, *, #19302, .T. ) ;
#8439=EDGE_CURVE ( 'NONE', #8203, #3887, #11371, .T. ) ;
#8453=CARTESIAN_POINT ( 'NONE',  ( -1.999999999999994449, 45.00000000000000000, -23.99999999999999645 ) ) ;
#8455=DIRECTION ( 'NONE',  ( 1.000000000000000000, -0.000000000000000000, -0.000000000000000000 ) ) ;
#8457=ORIENTED_EDGE ( 'NONE', *, *, #7777, .F. ) ;
#8458=CARTESIAN_POINT ( 'NONE',  ( -23.84999999999999432, -15.03999999999999915, -27.00000000000000000 ) ) ;
#8468=CARTESIAN_POINT ( 'NONE',  ( -23.89999999999999858, 29.50000000000000000, -27.00000000000000000 ) ) ;
#8471=ORIENTED_EDGE ( 'NONE', *, *, #5084, .T. ) ;
#8475=FACE_OUTER_BOUND ( 'NONE', #18269, .T. ) ;
#8476=CARTESIAN_POINT ( 'NONE',  ( -14.79187224938324974, -2.570168443617189880, -9.168425918763428939 ) ) ;
#8485=EDGE_CURVE ( 'NONE', #19575, #7696, #13903, .T. ) ;
#8486=VERTEX_POINT ( 'NONE', #19509 ) ;
#8491=CYLINDRICAL_SURFACE ( 'NONE', #22420, 5.100000000000000533 ) ;
#8499=ADVANCED_FACE ( 'NONE', ( #727 ), #4755, .F. ) ;
#8504=CARTESIAN_POINT ( 'NONE',  ( 30.44534269664589843, 40.40463133211081015, -27.00000000000000000 ) ) ;
#8507=CIRCLE ( 'NONE', #22939, 9.499999999999989342 ) ;
#8510=CARTESIAN_POINT ( 'NONE',  ( 0.000000000000000000, 45.00000000000000000, -27.00000000000000000 ) ) ;
#8517=DIRECTION ( 'NONE',  ( -1.000000000000000000, 0.000000000000000000, 0.000000000000000000 ) ) ;
#8535=DIRECTION ( 'NONE',  ( -4.613626265895764052E-16, -1.000000000000000000, 0.000000000000000000 ) ) ;
#8537=DIRECTION ( 'NONE',  ( 0.7071067811865660024, 8.659560562355159656E-17, -0.7071067811865291430 ) ) ;
#8547=ORIENTED_EDGE ( 'NONE', *, *, #9876, .T. ) ;
#8554=CARTESIAN_POINT ( 'NONE',  ( -2.024999999999999911, -45.00000000000000000, 27.00000000000000000 ) ) ;
#8557=ORIENTED_EDGE ( 'NONE', *, *, #6282, .F. ) ;
#8572=DIRECTION ( 'NONE',  ( 0.000000000000000000, 0.000000000000000000, 1.000000000000000000 ) ) ;
#8584=CARTESIAN_POINT ( 'NONE',  ( -17.38700629636781869, -8.908123924593986942, 3.336041480784321500 ) ) ;
#8589=DIRECTION ( 'NONE',  ( 0.4011779117250717785, -0.9160001545545232160, 0.000000000000000000 ) ) ;
#8593=CARTESIAN_POINT ( 'NONE',  ( 0.000000000000000000, 45.00000000000000000, -27.00000000000000000 ) ) ;
#8596=CARTESIAN_POINT ( 'NONE',  ( 17.19784311473119587, -8.411123426659415259, -4.422670359120409955 ) ) ;
#8600=DIRECTION ( 'NONE',  ( -0.000000000000000000, -0.000000000000000000, -1.000000000000000000 ) ) ;
#8614=LINE ( 'NONE', #7277, #12317 ) ;
#8618=DIRECTION ( 'NONE',  ( 4.613626265895763066E-16, 1.000000000000000000, 0.000000000000000000 ) ) ;
#8623=CARTESIAN_POINT ( 'NONE',  ( 0.000000000000000000, -45.00000000000000000, 23.99999999999999645 ) ) ;
#8638=AXIS2_PLACEMENT_3D ( 'NONE', #3164, #21839, #8535 ) ;
#8639=DIRECTION ( 'NONE',  ( -0.000000000000000000, -0.000000000000000000, -1.000000000000000000 ) ) ;
#8647=ORIENTED_EDGE ( 'NONE', *, *, #6530, .F. ) ;
#8650=DIRECTION ( 'NONE',  ( -0.000000000000000000, 0.000000000000000000, -1.000000000000000000 ) ) ;
#8654=ORIENTED_EDGE ( 'NONE', *, *, #1753, .T. ) ;
#8656=ORIENTED_EDGE ( 'NONE', *, *, #1014, .T. ) ;
#8661=VECTOR ( 'NONE', #9022, 1000.000000000000000 ) ;
#8663=VECTOR ( 'NONE', #18297, 1000.000000000000000 ) ;
#8667=DIRECTION ( 'NONE',  ( 0.000000000000000000, 0.000000000000000000, 1.000000000000000000 ) ) ;
#8669=VECTOR ( 'NONE', #22596, 1000.000000000000000 ) ;
#8695=CARTESIAN_POINT ( 'NONE',  ( -41.99999999999999289, 25.93535998569253920, -27.00000000000000000 ) ) ;
#8696=ADVANCED_FACE ( 'NONE', ( #5713 ), #20588, .F. ) ;
#8698=ORIENTED_EDGE ( 'NONE', *, *, #2826, .T. ) ;
#8702=ADVANCED_FACE ( 'NONE', ( #4116 ), #1805, .F. ) ;
#8703=VECTOR ( 'NONE', #13058, 1000.000000000000000 ) ;
#8709=EDGE_CURVE ( 'NONE', #9227, #2790, #7630, .T. ) ;
#8714=CARTESIAN_POINT ( 'NONE',  ( -17.32141611691247718, -8.728455122802975197, 3.780491077225288432 ) ) ;
#8715=CARTESIAN_POINT ( 'NONE',  ( -1.029124893018731811E-15, -45.00000000000000000, 22.79827876194487857 ) ) ;
#8723=CARTESIAN_POINT ( 'NONE',  ( 17.57831567727900079, -9.462949834988593878, 0.9681625741885133696 ) ) ;
#8730=CARTESIAN_POINT ( 'NONE',  ( -41.99999999999999289, 1.286185300804507526E-15, -10.50249999999999950 ) ) ;
#8746=DIRECTION ( 'NONE',  ( 0.000000000000000000, -1.000000000000000000, 0.000000000000000000 ) ) ;
#8754=DIRECTION ( 'NONE',  ( -0.000000000000000000, -0.000000000000000000, -1.000000000000000000 ) ) ;
#8762=SHAPE_REPRESENTATION ( 'Body', ( #8005 ), #20496 ) ;
#8771=VERTEX_POINT ( 'NONE', #3622 ) ;
#8781=CARTESIAN_POINT ( 'NONE',  ( 23.90000000000000568, 29.50000000000000000, 27.00000000000000000 ) ) ;
#8786=CARTESIAN_POINT ( 'NONE',  ( 20.85000000000000853, 15.03999999999999915, 27.00000000000000000 ) ) ;
#8796=CARTESIAN_POINT ( 'NONE',  ( -28.27483331787887266, 41.23752903419610760, -27.00000000000000000 ) ) ;
#8800=EDGE_CURVE ( 'NONE', #19379, #8820, #24008, .T. ) ;
#8801=DIRECTION ( 'NONE',  ( 1.000000000000000000, 0.000000000000000000, 0.000000000000000000 ) ) ;
#8812=DIRECTION ( 'NONE',  ( -1.000000000000000000, 0.000000000000000000, 0.000000000000000000 ) ) ;
#8813=CARTESIAN_POINT ( 'NONE',  ( 40.99749999999998096, 5.618459588085056979E-15, 0.000000000000000000 ) ) ;
#8820=VERTEX_POINT ( 'NONE', #4235 ) ;
#8830=ORIENTED_EDGE ( 'NONE', *, *, #22568, .T. ) ;
#8841=CARTESIAN_POINT ( 'NONE',  ( 0.000000000000000000, 0.000000000000000000, 27.00000000000000000 ) ) ;
#8846=CARTESIAN_POINT ( 'NONE',  ( 23.85000000000000497, 15.03999999999999915, -25.00000000000000000 ) ) ;
#8863=CARTESIAN_POINT ( 'NONE',  ( 20.85000000000000853, 15.03999999999999915, -25.00000000000000000 ) ) ;
#8872=CARTESIAN_POINT ( 'NONE',  ( 17.49232137458055192, 9.205685982891283814, -2.395442301836272936 ) ) ;
#8883=EDGE_LOOP ( 'NONE', ( #11410, #21849, #13951, #22480 ) ) ;
#8888=ORIENTED_EDGE ( 'NONE', *, *, #7793, .F. ) ;
#8894=LINE ( 'NONE', #5732, #16177 ) ;
#8911=DIRECTION ( 'NONE',  ( -0.000000000000000000, -0.000000000000000000, 1.000000000000000000 ) ) ;
#8924=EDGE_CURVE ( 'NONE', #22742, #22311, #8283, .T. ) ;
#8942=CARTESIAN_POINT ( 'NONE',  ( -14.80736872429922002, -4.130115634539735403, -8.564444421911375116 ) ) ;
#8944=CARTESIAN_POINT ( 'NONE',  ( 1.999999999999994449, 45.00000000000000000, -27.00000000000000000 ) ) ;
#8959=CARTESIAN_POINT ( 'NONE',  ( 41.99999999999999289, 25.93535998569253920, 27.00000000000000000 ) ) ;
#8961=ORIENTED_EDGE ( 'NONE', *, *, #6251, .T. ) ;
#8964=AXIS2_PLACEMENT_3D ( 'NONE', #6368, #11703, #16212 ) ;
#8997=ADVANCED_FACE ( 'NONE', ( #15225 ), #15869, .T. ) ;
#9013=LINE ( 'NONE', #3427, #19305 ) ;
#9022=DIRECTION ( 'NONE',  ( -0.7071067811865660024, 0.000000000000000000, -0.7071067811865291430 ) ) ;
#9026=CARTESIAN_POINT ( 'NONE',  ( -28.99999999999999645, 29.50000000000000000, -27.00000000000000000 ) ) ;
#9038=PLANE ( 'NONE',  #731 ) ;
#9045=CARTESIAN_POINT ( 'NONE',  ( 14.98950073861089294, -0.6491375924673296050, 9.483449329262333194 ) ) ;
#9059=LINE ( 'NONE', #5663, #12320 ) ;
#9060=ADVANCED_FACE ( 'NONE', ( #9131 ), #14973, .F. ) ;
#9078=CARTESIAN_POINT ( 'NONE',  ( -14.91624121966758842, 1.615102390220944706, -9.367332145225624629 ) ) ;
#9088=EDGE_CURVE ( 'NONE', #22311, #15590, #3527, .T. ) ;
#9091=ORIENTED_EDGE ( 'NONE', *, *, #2798, .F. ) ;
#9093=DIRECTION ( 'NONE',  ( -0.000000000000000000, -0.000000000000000000, -1.000000000000000000 ) ) ;
#9116=EDGE_CURVE ( 'NONE', #2505, #230, #11788, .T. ) ;
#9121=VECTOR ( 'NONE', #19115, 1000.000000000000000 ) ;
#9124=CARTESIAN_POINT ( 'NONE',  ( 40.89823313241238623, -26.41789760203348081, 27.00000000000000000 ) ) ;
#9131=FACE_OUTER_BOUND ( 'NONE', #301, .T. ) ;
#9148=EDGE_CURVE ( 'NONE', #22869, #8004, #17054, .T. ) ;
#9159=ORIENTED_EDGE ( 'NONE', *, *, #8076, .T. ) ;
#9160=VECTOR ( 'NONE', #15109, 1000.000000000000000 ) ;
#9167=ORIENTED_EDGE ( 'NONE', *, *, #10499, .T. ) ;
#9169=DIRECTION ( 'NONE',  ( 0.000000000000000000, 0.000000000000000000, 1.000000000000000000 ) ) ;
#9189=ORIENTED_EDGE ( 'NONE', *, *, #9707, .F. ) ;
#9206=CARTESIAN_POINT ( 'NONE',  ( -14.98952570844870102, 0.6468970097546546949, -9.483487670324119989 ) ) ;
#9225=ORIENTED_EDGE ( 'NONE', *, *, #18122, .T. ) ;
#9227=VERTEX_POINT ( 'NONE', #13262 ) ;
#9230=CARTESIAN_POINT ( 'NONE',  ( -14.99999999999999822, 0.000000000000000000, 27.00000000000000000 ) ) ;
#9246=DIRECTION ( 'NONE',  ( -0.000000000000000000, -0.000000000000000000, -1.000000000000000000 ) ) ;
#9264=( NAMED_UNIT ( * ) PLANE_ANGLE_UNIT ( ) SI_UNIT ( $, .RADIAN. ) );
#9272=ORIENTED_EDGE ( 'NONE', *, *, #1728, .F. ) ;
#9274=ADVANCED_FACE ( 'NONE', ( #21584 ), #16201, .F. ) ;
#9283=ORIENTED_EDGE ( 'NONE', *, *, #12704, .T. ) ;
#9289=ORIENTED_EDGE ( 'NONE', *, *, #11157, .T. ) ;
#9297=EDGE_CURVE ( 'NONE', #732, #5422, #16461, .T. ) ;
#9323=DIRECTION ( 'NONE',  ( -1.000000000000000000, 0.000000000000000000, 0.000000000000000000 ) ) ;
#9331=ORIENTED_EDGE ( 'NONE', *, *, #7253, .T. ) ;
#9334=DIRECTION ( 'NONE',  ( -1.000000000000000000, 0.000000000000000000, 0.000000000000000000 ) ) ;
#9335=CARTESIAN_POINT ( 'NONE',  ( 14.80736872429922357, 4.130115634539733627, -8.564444421911364458 ) ) ;
#9349=DIRECTION ( 'NONE',  ( -0.000000000000000000, -0.000000000000000000, 1.000000000000000000 ) ) ;
#9352=CARTESIAN_POINT ( 'NONE',  ( -17.49232137458055192, 9.205685982891283814, 2.395442301836276933 ) ) ;
#9371=ADVANCED_FACE ( 'NONE', ( #4631, #12033 ), #13002, .F. ) ;
#9379=EDGE_LOOP ( 'NONE', ( #18343, #3485, #18740, #1631 ) ) ;
#9383=CIRCLE ( 'NONE', #19173, 20.85000000000000853 ) ;
#9398=LINE ( 'NONE', #3935, #6026 ) ;
#9405=EDGE_LOOP ( 'NONE', ( #22404, #13818, #20983, #7586 ) ) ;
#9419=ORIENTED_EDGE ( 'NONE', *, *, #16535, .T. ) ;
#9426=AXIS2_PLACEMENT_3D ( 'NONE', #4139, #15802, #7877 ) ;
#9429=VECTOR ( 'NONE', #11197, 1000.000000000000000 ) ;
#9437=LINE ( 'NONE', #11031, #17296 ) ;
#9440=LINE ( 'NONE', #7491, #10824 ) ;
#9443=CIRCLE ( 'NONE', #23119, 23.85000000000000497 ) ;
#9447=AXIS2_PLACEMENT_3D ( 'NONE', #18128, #19940, #20190 ) ;
#9451=EDGE_CURVE ( 'NONE', #886, #7845, #14508, .T. ) ;
#9464=VERTEX_POINT ( 'NONE', #10806 ) ;
#9470=DIRECTION ( 'NONE',  ( -0.9160001545545232160, 0.4011779117250717785, -0.000000000000000000 ) ) ;
#9480=CARTESIAN_POINT ( 'NONE',  ( -17.38700629636782580, 8.908123924593990495, -3.336041480784321056 ) ) ;
#9486=FACE_OUTER_BOUND ( 'NONE', #23089, .T. ) ;
#9499=FACE_OUTER_BOUND ( 'NONE', #19539, .T. ) ;
#9501=CARTESIAN_POINT ( 'NONE',  ( 23.85000000000000497, 15.03999999999999915, -27.00000000000000000 ) ) ;
#9509=DIRECTION ( 'NONE',  ( 0.000000000000000000, 0.000000000000000000, 1.000000000000000000 ) ) ;
#9516=CARTESIAN_POINT ( 'NONE',  ( -20.85000000000000853, 15.04000000000000092, -25.00000000000000000 ) ) ;
#9578=CONICAL_SURFACE ( 'NONE', #1046, 10.50249999999999950, 0.7853981633974447263 ) ;
#9581=EDGE_CURVE ( 'NONE', #15077, #13001, #5170, .T. ) ;
#9593=VECTOR ( 'NONE', #1525, 1000.000000000000000 ) ;
#9611=EDGE_CURVE ( 'NONE', #13451, #18900, #14904, .T. ) ;
#9637=CARTESIAN_POINT ( 'NONE',  ( 14.98950073861089294, 0.6491375924673389308, -9.483449329262333194 ) ) ;
#9643=ORIENTED_EDGE ( 'NONE', *, *, #1949, .F. ) ;
#9648=AXIS2_PLACEMENT_3D ( 'NONE', #13364, #22773, #9689 ) ;
#9666=ORIENTED_EDGE ( 'NONE', *, *, #8709, .T. ) ;
#9668=CARTESIAN_POINT ( 'NONE',  ( -39.99999999999999289, 29.50000000000000000, 27.00000000000000000 ) ) ;
#9669=CARTESIAN_POINT ( 'NONE',  ( -1.999999999999994449, -45.00000000000000000, 26.97499999999999432 ) ) ;
#9670=VERTEX_POINT ( 'NONE', #15067 ) ;
#9671=ORIENTED_EDGE ( 'NONE', *, *, #19883, .F. ) ;
#9678=ORIENTED_EDGE ( 'NONE', *, *, #8163, .F. ) ;
#9680=ADVANCED_FACE ( 'NONE', ( #17028 ), #22645, .F. ) ;
#9685=DIRECTION ( 'NONE',  ( -0.000000000000000000, -0.000000000000000000, -1.000000000000000000 ) ) ;
#9687=LINE ( 'NONE', #7848, #22658 ) ;
#9689=DIRECTION ( 'NONE',  ( -1.000000000000000000, 0.000000000000000000, 0.000000000000000000 ) ) ;
#9691=DIRECTION ( 'NONE',  ( -0.000000000000000000, 0.000000000000000000, -1.000000000000000000 ) ) ;
#9693=ORIENTED_EDGE ( 'NONE', *, *, #19958, .T. ) ;
#9696=CARTESIAN_POINT ( 'NONE',  ( 17.15849686392983386, 8.309918483244988607, -4.628645577532790156 ) ) ;
#9707=EDGE_CURVE ( 'NONE', #5080, #6532, #19366, .T. ) ;
#9718=CARTESIAN_POINT ( 'NONE',  ( 41.99999999999999289, 25.93535998569253920, 27.00000000000000000 ) ) ;
#9754=DIRECTION ( 'NONE',  ( -1.000000000000000000, 0.000000000000000000, 0.000000000000000000 ) ) ;
#9756=EDGE_CURVE ( 'NONE', #22991, #13688, #2448, .T. ) ;
#9785=CIRCLE ( 'NONE', #22275, 18.50000000000000000 ) ;
#9803=CARTESIAN_POINT ( 'NONE',  ( 23.85000000000000497, 15.03999999999999915, 25.00000000000000000 ) ) ;
#9815=EDGE_LOOP ( 'NONE', ( #7809, #15992, #8086, #8698 ) ) ;
#9817=AXIS2_PLACEMENT_3D ( 'NONE', #21526, #4828, #2989 ) ;
#9832=AXIS2_PLACEMENT_3D ( 'NONE', #12799, #10946, #18419 ) ;
#9837=CIRCLE ( 'NONE', #18810, 1.500000000000001332 ) ;
#9840=ORIENTED_EDGE ( 'NONE', *, *, #8709, .F. ) ;
#9848=ORIENTED_EDGE ( 'NONE', *, *, #16363, .F. ) ;
#9869=CARTESIAN_POINT ( 'NONE',  ( 0.000000000000000000, -15.23000000000000220, 27.00000000000000000 ) ) ;
#9872=DIRECTION ( 'NONE',  ( 0.000000000000000000, 0.000000000000000000, 1.000000000000000000 ) ) ;
#9876=EDGE_CURVE ( 'NONE', #11779, #23352, #21157, .T. ) ;
#9880=VECTOR ( 'NONE', #8746, 1000.000000000000000 ) ;
#9881=DIRECTION ( 'NONE',  ( -0.000000000000000000, -0.000000000000000000, -1.000000000000000000 ) ) ;
#9893=B_SPLINE_CURVE_WITH_KNOTS ( 'NONE', 3,
 ( #6416, #13860, #8476, #17390, #10300, #17882, #11997, #19469 ),
 .UNSPECIFIED., .F., .F.,
 ( 4, 2, 2, 4 ),
 ( 1.734723475976807094E-18, 0.001946159586596642828, 0.002919239379894964133, 0.003892319173193285655 ),
 .UNSPECIFIED. ) ;
#9903=FACE_OUTER_BOUND ( 'NONE', #2370, .T. ) ;
#9911=CIRCLE ( 'NONE', #585, 1.500000000000001332 ) ;
#9930=EDGE_CURVE ( 'NONE', #22874, #17607, #9443, .T. ) ;
#9952=VECTOR ( 'NONE', #11548, 1000.000000000000000 ) ;
#9957=CIRCLE ( 'NONE', #1799, 23.84999999999999432 ) ;
#9959=DIRECTION ( 'NONE',  ( 4.613626265895764052E-16, 1.000000000000000000, 0.000000000000000000 ) ) ;
#9968=EDGE_CURVE ( 'NONE', #19120, #18612, #12196, .T. ) ;
#9978=LINE ( 'NONE', #2800, #17702 ) ;
#9983=DIRECTION ( 'NONE',  ( 0.000000000000000000, 0.000000000000000000, 1.000000000000000000 ) ) ;
#9994=DIRECTION ( 'NONE',  ( 1.000000000000000000, 0.000000000000000000, 0.000000000000000000 ) ) ;
#10013=EDGE_LOOP ( 'NONE', ( #9289, #14679, #9848, #15474 ) ) ;
#10030=ORIENTED_EDGE ( 'NONE', *, *, #8432, .T. ) ;
#10047=CARTESIAN_POINT ( 'NONE',  ( -14.51962751333974389, 3.765689428759031010, -27.00000000000000000 ) ) ;
#10051=DIRECTION ( 'NONE',  ( -0.000000000000000000, -0.000000000000000000, 1.000000000000000000 ) ) ;
#10066=ORIENTED_EDGE ( 'NONE', *, *, #20336, .F. ) ;
#10072=ADVANCED_FACE ( 'NONE', ( #19895, #18196 ), #14276, .T. ) ;
#10081=EDGE_LOOP ( 'NONE', ( #3634, #720, #683, #23950 ) ) ;
#10099=LINE ( 'NONE', #19780, #13453 ) ;
#10108=DIRECTION ( 'NONE',  ( -0.000000000000000000, -0.000000000000000000, -1.000000000000000000 ) ) ;
#10112=CIRCLE ( 'NONE', #19886, 49.99999999999999289 ) ;
#10139=ORIENTED_EDGE ( 'NONE', *, *, #3707, .F. ) ;
#10147=EDGE_CURVE ( 'NONE', #18900, #20705, #19671, .T. ) ;
#10150=CARTESIAN_POINT ( 'NONE',  ( 0.000000000000000000, 0.000000000000000000, -27.00000000000000000 ) ) ;
#10154=ORIENTED_EDGE ( 'NONE', *, *, #2761, .F. ) ;
#10155=MANIFOLD_SOLID_BREP ( 'Mirror3', #7726 ) ;
#10156=ORIENTED_EDGE ( 'NONE', *, *, #14171, .T. ) ;
#10158=FACE_BOUND ( 'NONE', #11293, .T. ) ;
#10164=CARTESIAN_POINT ( 'NONE',  ( -16.36913330654531507, -6.602951766536811817, -6.845624079409802221 ) ) ;
#10173=CARTESIAN_POINT ( 'NONE',  ( -23.84999999999999432, -15.03999999999999915, 25.00000000000000000 ) ) ;
#10175=CARTESIAN_POINT ( 'NONE',  ( 17.57797814737053699, -9.461914562436907872, -0.9781177603712922775 ) ) ;
#10176=CARTESIAN_POINT ( 'NONE',  ( -28.99999999999999645, -29.50000000000001066, 27.00000000000000000 ) ) ;
#10179=EDGE_CURVE ( 'NONE', #12687, #14244, #3779, .T. ) ;
#10192=CARTESIAN_POINT ( 'NONE',  ( -18.50000000000000000, 15.23000000000000220, -27.00000000000000000 ) ) ;
#10194=DIRECTION ( 'NONE',  ( 1.000000000000000000, 0.000000000000000000, 0.000000000000000000 ) ) ;
#10200=CIRCLE ( 'NONE', #13317, 18.50000000000000000 ) ;
#10206=CARTESIAN_POINT ( 'NONE',  ( 0.000000000000000000, 45.00000000000000000, -27.00000000000000000 ) ) ;
#10210=DIRECTION ( 'NONE',  ( 1.000000000000000000, 0.000000000000000000, 0.000000000000000000 ) ) ;
#10223=AXIS2_PLACEMENT_3D ( 'NONE', #16672, #12644, #5567 ) ;
#10233=LINE ( 'NONE', #4654, #21540 ) ;
#10235=ADVANCED_FACE ( 'NONE', ( #20256 ), #16452, .F. ) ;
#10247=VERTEX_POINT ( 'NONE', #2054 ) ;
#10259=VECTOR ( 'NONE', #9246, 1000.000000000000000 ) ;
#10264=CARTESIAN_POINT ( 'NONE',  ( 40.89823313241237912, 26.41789760203348081, 27.00000000000000000 ) ) ;
#10267=AXIS2_PLACEMENT_3D ( 'NONE', #8334, #6032, #4695 ) ;
#10270=CIRCLE ( 'NONE', #23926, 49.99999999999999289 ) ;
#10271=LINE ( 'NONE', #16005, #15350 ) ;
#10282=CARTESIAN_POINT ( 'NONE',  ( -28.99999999999999645, 29.50000000000000000, 27.00000000000000000 ) ) ;
#10295=CIRCLE ( 'NONE', #16534, 2.024999999999999911 ) ;
#10297=ORIENTED_EDGE ( 'NONE', *, *, #18584, .T. ) ;
#10300=CARTESIAN_POINT ( 'NONE',  ( -14.94708199919714176, -1.300481340138141872, -9.416259293296521449 ) ) ;
#10319=AXIS2_PLACEMENT_3D ( 'NONE', #1902, #1449, #18501 ) ;
#10340=DIRECTION ( 'NONE',  ( 1.000000000000000000, 0.000000000000000000, 0.000000000000000000 ) ) ;
#10343=DIRECTION ( 'NONE',  ( -0.000000000000000000, -0.000000000000000000, -1.000000000000000000 ) ) ;
#10344=CARTESIAN_POINT ( 'NONE',  ( -14.51962751333973856, 3.765689428759025681, 8.721787840009204373 ) ) ;
#10351=ORIENTED_EDGE ( 'NONE', *, *, #11463, .F. ) ;
#10376=DIRECTION ( 'NONE',  ( -0.000000000000000000, -0.000000000000000000, -1.000000000000000000 ) ) ;
#10383=LINE ( 'NONE', #16346, #20451 ) ;
#10388=FACE_OUTER_BOUND ( 'NONE', #12330, .T. ) ;
#10393=AXIS2_PLACEMENT_3D ( 'NONE', #9124, #20134, #18049 ) ;
#10404=CARTESIAN_POINT ( 'NONE',  ( -28.99999999999999645, -29.50000000000001066, 27.00000000000000000 ) ) ;
#10414=ORIENTED_EDGE ( 'NONE', *, *, #1728, .T. ) ;
#10416=CARTESIAN_POINT ( 'NONE',  ( 23.90000000000000924, -29.50000000000000711, 27.00000000000000000 ) ) ;
#10419=EDGE_LOOP ( 'NONE', ( #8830, #14999, #15692, #17857 ) ) ;
#10421=CARTESIAN_POINT ( 'NONE',  ( -1.999999999999994449, -45.00000000000000000, 27.00000000000000000 ) ) ;
#10423=DIRECTION ( 'NONE',  ( -1.000000000000000000, 0.000000000000000000, 0.000000000000000000 ) ) ;
#10424=DIRECTION ( 'NONE',  ( -1.000000000000000000, 0.000000000000000000, 0.000000000000000000 ) ) ;
#10425=B_SPLINE_CURVE_WITH_KNOTS ( 'NONE', 3,
 ( #15934, #23281, #6556, #10436, #6434, #16044, #4725, #17634 ),
 .UNSPECIFIED., .F., .F.,
 ( 4, 2, 2, 4 ),
 ( 0.003892319173193294762, 0.004864202078960318081, 0.005836084984727341399, 0.007779850796261386300 ),
 .UNSPECIFIED. ) ;
#10427=ORIENTED_EDGE ( 'NONE', *, *, #9968, .F. ) ;
#10428=FACE_OUTER_BOUND ( 'NONE', #15647, .T. ) ;
#10431=DIRECTION ( 'NONE',  ( -1.000000000000000000, 0.000000000000000000, 0.000000000000000000 ) ) ;
#10436=CARTESIAN_POINT ( 'NONE',  ( 14.94777716362148645, 1.291632522116896054, 9.417361603030277806 ) ) ;
#10438=EDGE_CURVE ( 'NONE', #5080, #498, #23176, .T. ) ;
#10441=ORIENTED_EDGE ( 'NONE', *, *, #21704, .T. ) ;
#10446=ADVANCED_FACE ( 'NONE', ( #19270 ), #8134, .F. ) ;
#10468=ORIENTED_EDGE ( 'NONE', *, *, #10596, .T. ) ;
#10489=CYLINDRICAL_SURFACE ( 'NONE', #19093, 4.999999999999997335 ) ;
#10491=LINE ( 'NONE', #20261, #17751 ) ;
#10499=EDGE_CURVE ( 'NONE', #19529, #10789, #6938, .T. ) ;
#10501=DIRECTION ( 'NONE',  ( -0.000000000000000000, -0.000000000000000000, -1.000000000000000000 ) ) ;
#10508=ORIENTED_EDGE ( 'NONE', *, *, #10655, .T. ) ;
#10512=CARTESIAN_POINT ( 'NONE',  ( -39.99999999999999289, -29.50000000000001066, 27.00000000000000000 ) ) ;
#10520=FACE_OUTER_BOUND ( 'NONE', #19633, .T. ) ;
#10530=DIRECTION ( 'NONE',  ( -1.000000000000000000, 0.000000000000000000, 0.000000000000000000 ) ) ;
#10537=DIRECTION ( 'NONE',  ( 0.9160001545545232160, 0.4011779117250717785, 0.000000000000000000 ) ) ;
#10540=FACE_OUTER_BOUND ( 'NONE', #5382, .T. ) ;
#10542=CARTESIAN_POINT ( 'NONE',  ( 17.49066032632880408, -9.200828712690857003, -2.414248458042545842 ) ) ;
#10565=ADVANCED_FACE ( 'NONE', ( #3269 ), #21709, .F. ) ;
#10568=DIRECTION ( 'NONE',  ( 1.000000000000000000, 0.000000000000000000, 0.000000000000000000 ) ) ;
#10571=CARTESIAN_POINT ( 'NONE',  ( 17.19784311473120653, 8.411123426659424140, 4.422670359120418837 ) ) ;
#10596=EDGE_CURVE ( 'NONE', #6874, #5306, #17226, .T. ) ;
#10599=DIRECTION ( 'NONE',  ( -1.000000000000000000, 0.000000000000000000, 0.000000000000000000 ) ) ;
#10603=ORIENTED_EDGE ( 'NONE', *, *, #18122, .F. ) ;
#10606=AXIS2_PLACEMENT_3D ( 'NONE', #12875, #20333, #20459 ) ;
#10607=CARTESIAN_POINT ( 'NONE',  ( 20.85000000000000853, 15.03999999999999915, 25.00000000000000000 ) ) ;
#10608=AXIS2_PLACEMENT_3D ( 'NONE', #636, #9872, #6607 ) ;
#10626=ADVANCED_FACE ( 'NONE', ( #2785 ), #2776, .F. ) ;
#10629=CARTESIAN_POINT ( 'NONE',  ( 28.27483331787888332, -41.23752903419610050, 27.00000000000000000 ) ) ;
#10631=VERTEX_POINT ( 'NONE', #7162 ) ;
#10633=FACE_OUTER_BOUND ( 'NONE', #3574, .T. ) ;
#10640=DIRECTION ( 'NONE',  ( 0.000000000000000000, -1.000000000000000000, 0.000000000000000000 ) ) ;
#10652=CARTESIAN_POINT ( 'NONE',  ( 0.000000000000000000, -45.00000000000000000, -23.99999999999999645 ) ) ;
#10655=EDGE_CURVE ( 'NONE', #17886, #22869, #5882, .T. ) ;
#10663=DIRECTION ( 'NONE',  ( -0.000000000000000000, -1.000000000000000000, -0.000000000000000000 ) ) ;
#10682=EDGE_CURVE ( 'NONE', #10927, #3165, #18358, .T. ) ;
#10683=AXIS2_PLACEMENT_3D ( 'NONE', #5850, #1840, #10844 ) ;
#10687=CIRCLE ( 'NONE', #5258, 5.100000000000000533 ) ;
#10691=VECTOR ( 'NONE', #18040, 1000.000000000000000 ) ;
#10694=DIRECTION ( 'NONE',  ( 0.000000000000000000, 0.000000000000000000, 1.000000000000000000 ) ) ;
#10696=CARTESIAN_POINT ( 'NONE',  ( 16.18147534945000032, 6.260849737139247750, 7.148624562014526340 ) ) ;
#10712=CIRCLE ( 'NONE', #19693, 14.99999999999999822 ) ;
#10737=CARTESIAN_POINT ( 'NONE',  ( -1.999999999999994449, 45.00000000000000000, 26.97499999999999432 ) ) ;
#10750=CARTESIAN_POINT ( 'NONE',  ( -31.10231664966676135, -45.36128193761570770, 27.00000000000000000 ) ) ;
#10757=AXIS2_PLACEMENT_3D ( 'NONE', #2867, #5173, #15919 ) ;
#10761=CARTESIAN_POINT ( 'NONE',  ( 0.000000000000000000, -15.23000000000000220, 27.00000000000000000 ) ) ;
#10770=AXIS2_PLACEMENT_3D ( 'NONE', #14649, #16124, #14399 ) ;
#10771=LINE ( 'NONE', #9501, #19655 ) ;
#10772=DIRECTION ( 'NONE',  ( -1.000000000000000000, 0.000000000000000000, 0.000000000000000000 ) ) ;
#10789=VERTEX_POINT ( 'NONE', #8107 ) ;
#10802=DIRECTION ( 'NONE',  ( -1.000000000000000000, 0.000000000000000000, 0.000000000000000000 ) ) ;
#10806=CARTESIAN_POINT ( 'NONE',  ( -1.029124893018731811E-15, 45.00000000000000000, 22.79827876194487857 ) ) ;
#10814=VERTEX_POINT ( 'NONE', #6181 ) ;
#10818=EDGE_LOOP ( 'NONE', ( #15549, #6564, #20550, #4957, #5136, #259 ) ) ;
#10824=VECTOR ( 'NONE', #20945, 1000.000000000000000 ) ;
#10829=LINE ( 'NONE', #20137, #12967 ) ;
#10830=CARTESIAN_POINT ( 'NONE',  ( -2.024999999999999911, 45.00000000000000000, 27.00000000000000000 ) ) ;
#10831=LINE ( 'NONE', #3646, #8663 ) ;
#10834=ORIENTED_EDGE ( 'NONE', *, *, #4738, .T. ) ;
#10844=DIRECTION ( 'NONE',  ( -1.000000000000000000, 0.000000000000000000, 0.000000000000000000 ) ) ;
#10848=EDGE_CURVE ( 'NONE', #3277, #17283, #13241, .T. ) ;
#10855=CYLINDRICAL_SURFACE ( 'NONE', #6072, 23.85000000000000497 ) ;
#10864=CARTESIAN_POINT ( 'NONE',  ( -28.99999999999999645, 29.50000000000000000, 27.00000000000000000 ) ) ;
#10869=LINE ( 'NONE', #17869, #23553 ) ;
#10881=EDGE_LOOP ( 'NONE', ( #12478, #17128, #6517, #20473 ) ) ;
#10903=CARTESIAN_POINT ( 'NONE',  ( 23.84999999999999432, -15.03999999999999559, 25.00000000000000000 ) ) ;
#10910=ADVANCED_FACE ( 'NONE', ( #17893 ), #23829, .F. ) ;
#10914=CARTESIAN_POINT ( 'NONE',  ( 23.85000000000000497, 15.03999999999999915, 25.00000000000000000 ) ) ;
#10917=CARTESIAN_POINT ( 'NONE',  ( 17.32314925601269451, 8.733074366907754182, -3.769949228126190377 ) ) ;
#10927=VERTEX_POINT ( 'NONE', #18004 ) ;
#10934=EDGE_CURVE ( 'NONE', #8356, #23464, #23279, .T. ) ;
#10940=EDGE_CURVE ( 'NONE', #17886, #10927, #12011, .T. ) ;
#10946=DIRECTION ( 'NONE',  ( 0.000000000000000000, 0.000000000000000000, 1.000000000000000000 ) ) ;
#10950=ORIENTED_EDGE ( 'NONE', *, *, #7503, .F. ) ;
#10958=VECTOR ( 'NONE', #18661, 1000.000000000000000 ) ;
#10959=AXIS2_PLACEMENT_3D ( 'NONE', #18635, #11398, #18873 ) ;
#10972=ORIENTED_EDGE ( 'NONE', *, *, #21052, .F. ) ;
#10984=ORIENTED_EDGE ( 'NONE', *, *, #21227, .F. ) ;
#10988=EDGE_CURVE ( 'NONE', #128, #2676, #8224, .T. ) ;
#10991=CIRCLE ( 'NONE', #10608, 18.50000000000000000 ) ;
#10993=VECTOR ( 'NONE', #297, 999.9999999999998863 ) ;
#11000=CARTESIAN_POINT ( 'NONE',  ( -20.85000000000000853, 15.04000000000000092, 27.00000000000000000 ) ) ;
#11018=ORIENTED_EDGE ( 'NONE', *, *, #22246, .T. ) ;
#11031=CARTESIAN_POINT ( 'NONE',  ( 23.85000000000000497, 15.03999999999999915, 27.00000000000000000 ) ) ;
#11039=DIRECTION ( 'NONE',  ( 4.613626265895764052E-16, 1.000000000000000000, -0.000000000000000000 ) ) ;
#11042=CARTESIAN_POINT ( 'NONE',  ( -30.44534269664590198, 40.40463133211079594, 27.00000000000000000 ) ) ;
#11078=DIRECTION ( 'NONE',  ( -0.000000000000000000, -0.000000000000000000, -1.000000000000000000 ) ) ;
#11092=AXIS2_PLACEMENT_3D ( 'NONE', #21861, #7208, #3186 ) ;
#11097=ORIENTED_EDGE ( 'NONE', *, *, #10179, .F. ) ;
#11100=EDGE_LOOP ( 'NONE', ( #1571, #2311, #2230, #19773 ) ) ;
#11101=CYLINDRICAL_SURFACE ( 'NONE', #21559, 15.00000000000000000 ) ;
#11137=CARTESIAN_POINT ( 'NONE',  ( -14.67173559926288107, 3.179195828807836133, -8.975010320294703803 ) ) ;
#11157=EDGE_CURVE ( 'NONE', #7696, #8820, #7823, .T. ) ;
#11165=LINE ( 'NONE', #449, #2069 ) ;
#11183=CARTESIAN_POINT ( 'NONE',  ( 0.000000000000000000, 15.03999999999999915, -27.00000000000000000 ) ) ;
#11185=DIRECTION ( 'NONE',  ( -1.000000000000000000, 0.000000000000000000, 0.000000000000000000 ) ) ;
#11190=ADVANCED_FACE ( 'NONE', ( #4450 ), #17111, .F. ) ;
#11192=AXIS2_PLACEMENT_3D ( 'NONE', #5340, #3139, #1556 ) ;
#11194=VERTEX_POINT ( 'NONE', #4317 ) ;
#11197=DIRECTION ( 'NONE',  ( -1.000000000000000000, -0.000000000000000000, -0.000000000000000000 ) ) ;
#11208=ORIENTED_EDGE ( 'NONE', *, *, #13056, .F. ) ;
#11209=CARTESIAN_POINT ( 'NONE',  ( 0.000000000000000000, 45.00000000000000000, -23.99999999999999645 ) ) ;
#11220=DIRECTION ( 'NONE',  ( -0.000000000000000000, -0.000000000000000000, -1.000000000000000000 ) ) ;
#11237=ORIENTED_EDGE ( 'NONE', *, *, #20698, .F. ) ;
#11240=EDGE_CURVE ( 'NONE', #11923, #1960, #18376, .T. ) ;
#11271=DIRECTION ( 'NONE',  ( -0.000000000000000000, -0.000000000000000000, -1.000000000000000000 ) ) ;
#11272=CARTESIAN_POINT ( 'NONE',  ( 16.19099482616364583, 6.271157271432194591, -7.149633965064781549 ) ) ;
#11292=CARTESIAN_POINT ( 'NONE',  ( -28.99999999999999645, 29.50000000000000000, 27.00000000000000000 ) ) ;
#11293=EDGE_LOOP ( 'NONE', ( #20244, #17934 ) ) ;
#11298=CARTESIAN_POINT ( 'NONE',  ( 20.85000000000000853, 15.03999999999999915, -25.00000000000000000 ) ) ;
#11313=LINE ( 'NONE', #6218, #15023 ) ;
#11326=DIRECTION ( 'NONE',  ( -1.000000000000000000, 0.000000000000000000, 0.000000000000000000 ) ) ;
#11331=AXIS2_PLACEMENT_3D ( 'NONE', #7821, #17234, #4080 ) ;
#11349=CARTESIAN_POINT ( 'NONE',  ( -28.99999999999999645, -29.50000000000001066, 27.00000000000000000 ) ) ;
#11353=VECTOR ( 'NONE', #23701, 1000.000000000000000 ) ;
#11354=EDGE_LOOP ( 'NONE', ( #13971, #9666, #10984, #23842 ) ) ;
#11371=CIRCLE ( 'NONE', #22707, 20.85000000000000853 ) ;
#11378=ORIENTED_EDGE ( 'NONE', *, *, #4905, .T. ) ;
#11396=DIRECTION ( 'NONE',  ( 0.000000000000000000, 0.000000000000000000, 1.000000000000000000 ) ) ;
#11398=DIRECTION ( 'NONE',  ( 1.000000000000000000, 0.000000000000000000, -0.000000000000000000 ) ) ;
#11399=CARTESIAN_POINT ( 'NONE',  ( 16.36913330654532217, 6.602951766536810041, -6.845624079409801332 ) ) ;
#11401=VECTOR ( 'NONE', #11220, 1000.000000000000000 ) ;
#11406=EDGE_LOOP ( 'NONE', ( #17817, #3872 ) ) ;
#11410=ORIENTED_EDGE ( 'NONE', *, *, #8287, .T. ) ;
#11411=AXIS2_PLACEMENT_3D ( 'NONE', #11298, #14979, #18662 ) ;
#11413=FACE_OUTER_BOUND ( 'NONE', #1448, .T. ) ;
#11417=CIRCLE ( 'NONE', #13784, 18.50000000000000000 ) ;
#11426=CARTESIAN_POINT ( 'NONE',  ( -39.99999999999999289, -27.79189783386527779, -27.00000000000000000 ) ) ;
#11441=CIRCLE ( 'NONE', #13803, 5.100000000000000533 ) ;
#11447=DIRECTION ( 'NONE',  ( 1.000000000000000000, 4.613626265895764052E-16, -0.000000000000000000 ) ) ;
#11452=VERTEX_POINT ( 'NONE', #15221 ) ;
#11463=EDGE_CURVE ( 'NONE', #569, #886, #17446, .T. ) ;
#11473=CARTESIAN_POINT ( 'NONE',  ( 20.85000000000000853, 15.03999999999999915, -25.00000000000000000 ) ) ;
#11480=ORIENTED_EDGE ( 'NONE', *, *, #3572, .F. ) ;
#11484=AXIS2_PLACEMENT_3D ( 'NONE', #17820, #850, #14138 ) ;
#11510=ORIENTED_EDGE ( 'NONE', *, *, #11902, .F. ) ;
#11514=EDGE_LOOP ( 'NONE', ( #15822, #3020, #6265, #17219 ) ) ;
#11517=AXIS2_PLACEMENT_3D ( 'NONE', #15837, #11782, #6307 ) ;
#11523=CARTESIAN_POINT ( 'NONE',  ( 41.99999999999999289, 5.618459588085056979E-15, 0.000000000000000000 ) ) ;
#11526=CIRCLE ( 'NONE', #21695, 20.85000000000000142 ) ;
#11530=DIRECTION ( 'NONE',  ( 1.000000000000000000, 0.000000000000000000, 0.000000000000000000 ) ) ;
#11548=DIRECTION ( 'NONE',  ( -0.000000000000000000, -0.000000000000000000, -1.000000000000000000 ) ) ;
#11555=EDGE_LOOP ( 'NONE', ( #18291, #2152, #3400, #13350, #13553, #14288 ) ) ;
#11562=DIRECTION ( 'NONE',  ( -0.000000000000000000, -0.000000000000000000, -1.000000000000000000 ) ) ;
#11579=CARTESIAN_POINT ( 'NONE',  ( 40.00000000000000000, -27.79189783386526358, 27.00000000000000000 ) ) ;
#11602=EDGE_CURVE ( 'NONE', #18617, #7700, #21610, .T. ) ;
#11604=VERTEX_POINT ( 'NONE', #2805 ) ;
#11610=EDGE_LOOP ( 'NONE', ( #10139, #11992 ) ) ;
#11611=CARTESIAN_POINT ( 'NONE',  ( -28.99999999999999645, -29.50000000000001066, 27.00000000000000000 ) ) ;
#11613=ORIENTED_EDGE ( 'NONE', *, *, #19724, .T. ) ;
#11651=ORIENTED_EDGE ( 'NONE', *, *, #18584, .F. ) ;
#11655=FACE_OUTER_BOUND ( 'NONE', #19879, .T. ) ;
#11656=CARTESIAN_POINT ( 'NONE',  ( 0.000000000000000000, 15.03999999999999915, -25.00000000000000000 ) ) ;
#11659=CARTESIAN_POINT ( 'NONE',  ( -1.999999999999994449, -45.00000000000000000, -26.97499999999999432 ) ) ;
#11662=EDGE_CURVE ( 'NONE', #6532, #18820, #10233, .T. ) ;
#11663=VERTEX_POINT ( 'NONE', #8781 ) ;
#11670=DIRECTION ( 'NONE',  ( -0.000000000000000000, -0.000000000000000000, -1.000000000000000000 ) ) ;
#11693=ORIENTED_EDGE ( 'NONE', *, *, #13137, .F. ) ;
#11699=LINE ( 'NONE', #8165, #7119 ) ;
#11703=DIRECTION ( 'NONE',  ( -0.000000000000000000, -0.000000000000000000, -1.000000000000000000 ) ) ;
#11719=DIRECTION ( 'NONE',  ( -0.8571673007021116675, 0.000000000000000000, -0.5150380749100552658 ) ) ;
#11750=ORIENTED_EDGE ( 'NONE', *, *, #21250, .F. ) ;
#11763=PLANE ( 'NONE',  #23930 ) ;
#11766=VECTOR ( 'NONE', #17923, 1000.000000000000000 ) ;
#11769=CIRCLE ( 'NONE', #20762, 5.100000000000000533 ) ;
#11773=VECTOR ( 'NONE', #15910, 1000.000000000000114 ) ;
#11776=CIRCLE ( 'NONE', #4012, 5.100000000000000533 ) ;
#11777=ORIENTED_EDGE ( 'NONE', *, *, #12876, .F. ) ;
#11779=VERTEX_POINT ( 'NONE', #14627 ) ;
#11782=DIRECTION ( 'NONE',  ( -0.000000000000000000, -0.000000000000000000, 1.000000000000000000 ) ) ;
#11785=AXIS2_PLACEMENT_3D ( 'NONE', #8424, #19536, #17699 ) ;
#11786=AXIS2_PLACEMENT_3D ( 'NONE', #16515, #16381, #10772 ) ;
#11788=LINE ( 'NONE', #352, #14867 ) ;
#11792=LINE ( 'NONE', #7035, #7094 ) ;
#11801=( GEOMETRIC_REPRESENTATION_CONTEXT ( 3 ) GLOBAL_UNCERTAINTY_ASSIGNED_CONTEXT ( ( #2775 ) ) GLOBAL_UNIT_ASSIGNED_CONTEXT ( ( #14153, #12907, #5482 ) ) REPRESENTATION_CONTEXT ( 'NONE', 'WORKASPACE' ) );
#11803=EDGE_CURVE ( 'NONE', #13831, #21442, #3415, .T. ) ;
#11807=ORIENTED_EDGE ( 'NONE', *, *, #13782, .F. ) ;
#11809=DIRECTION ( 'NONE',  ( -0.9160001545545232160, 0.4011779117250717785, -0.000000000000000000 ) ) ;
#11821=CARTESIAN_POINT ( 'NONE',  ( 0.000000000000000000, 15.03999999999999915, 25.00000000000000000 ) ) ;
#11827=CARTESIAN_POINT ( 'NONE',  ( 14.67187117805616303, 3.178673068337433349, -8.975236025575915377 ) ) ;
#11833=AXIS2_PLACEMENT_3D ( 'NONE', #15432, #19104, #17260 ) ;
#11836=EDGE_CURVE ( 'NONE', #2505, #5790, #10831, .T. ) ;
#11850=ORIENTED_EDGE ( 'NONE', *, *, #13056, .T. ) ;
#11857=VERTEX_POINT ( 'NONE', #1705 ) ;
#11881=AXIS2_PLACEMENT_3D ( 'NONE', #3308, #18200, #1493 ) ;
#11886=VERTEX_POINT ( 'NONE', #5479 ) ;
#11890=DIRECTION ( 'NONE',  ( -0.000000000000000000, -0.000000000000000000, 1.000000000000000000 ) ) ;
#11896=CARTESIAN_POINT ( 'NONE',  ( -39.99999999999999289, -29.50000000000001066, 27.00000000000000000 ) ) ;
#11899=CARTESIAN_POINT ( 'NONE',  ( 17.59041996266972063, -9.500503876990118002, 0.4759723220310708713 ) ) ;
#11902=EDGE_CURVE ( 'NONE', #16743, #4095, #116, .T. ) ;
#11903=FACE_OUTER_BOUND ( 'NONE', #13278, .T. ) ;
#11906=VECTOR ( 'NONE', #15433, 1000.000000000000000 ) ;
#11910=EDGE_LOOP ( 'NONE', ( #20323, #16082, #14342, #20789 ) ) ;
#11911=DIRECTION ( 'NONE',  ( -0.000000000000000000, -0.000000000000000000, 1.000000000000000000 ) ) ;
#11915=CYLINDRICAL_SURFACE ( 'NONE', #5998, 1.999999999999994449 ) ;
#11923=VERTEX_POINT ( 'NONE', #5728 ) ;
#11930=DIRECTION ( 'NONE',  ( -0.000000000000000000, -0.000000000000000000, 1.000000000000000000 ) ) ;
#11944=CARTESIAN_POINT ( 'NONE',  ( 15.00000000000000000, 5.618453542512190434E-15, -9.499999999999987566 ) ) ;
#11955=CARTESIAN_POINT ( 'NONE',  ( 39.99999999999999289, 27.79189783386526358, 27.00000000000000000 ) ) ;
#11961=ORIENTED_EDGE ( 'NONE', *, *, #18944, .T. ) ;
#11962=FACE_OUTER_BOUND ( 'NONE', #22011, .T. ) ;
#11973=ADVANCED_FACE ( 'NONE', ( #2295 ), #5952, .F. ) ;
#11974=EDGE_CURVE ( 'NONE', #15590, #3047, #4004, .T. ) ;
#11984=CARTESIAN_POINT ( 'NONE',  ( 0.000000000000000000, 15.03999999999999915, -25.00000000000000000 ) ) ;
#11992=ORIENTED_EDGE ( 'NONE', *, *, #6127, .F. ) ;
#11994=VERTEX_POINT ( 'NONE', #7648 ) ;
#11997=CARTESIAN_POINT ( 'NONE',  ( -14.99999999999999822, -0.3242076166095216316, -9.499999999999994671 ) ) ;
#12000=CARTESIAN_POINT ( 'NONE',  ( -14.51962751333974033, -3.765689428759031010, 8.721787840009202597 ) ) ;
#12002=ADVANCED_FACE ( 'NONE', ( #2746 ), #21419, .F. ) ;
#12011=LINE ( 'NONE', #6552, #12908 ) ;
#12012=CARTESIAN_POINT ( 'NONE',  ( 16.36913330654531507, -6.602951766536811817, 6.845624079409791563 ) ) ;
#12021=LINE ( 'NONE', #19254, #5831 ) ;
#12030=ORIENTED_EDGE ( 'NONE', *, *, #63, .F. ) ;
#12033=FACE_OUTER_BOUND ( 'NONE', #18048, .T. ) ;
#12040=AXIS2_PLACEMENT_3D ( 'NONE', #19596, #23499, #1060 ) ;
#12060=ORIENTED_EDGE ( 'NONE', *, *, #10147, .F. ) ;
#12063=CARTESIAN_POINT ( 'NONE',  ( -39.99999999999999289, -29.50000000000001066, 27.00000000000000000 ) ) ;
#12071=ORIENTED_EDGE ( 'NONE', *, *, #20741, .T. ) ;
#12077=CARTESIAN_POINT ( 'NONE',  ( 34.10000000000001563, -29.50000000000000711, 27.00000000000000000 ) ) ;
#12082=EDGE_LOOP ( 'NONE', ( #22594, #21044 ) ) ;
#12093=DIRECTION ( 'NONE',  ( 1.000000000000000000, 0.000000000000000000, 0.000000000000000000 ) ) ;
#12094=CARTESIAN_POINT ( 'NONE',  ( -14.99999999999999822, 0.000000000000000000, 27.00000000000000000 ) ) ;
#12097=EDGE_LOOP ( 'NONE', ( #10468, #18960, #11208, #785 ) ) ;
#12106=EDGE_CURVE ( 'NONE', #2619, #8063, #15308, .T. ) ;
#12108=ORIENTED_EDGE ( 'NONE', *, *, #21912, .F. ) ;
#12115=DIRECTION ( 'NONE',  ( -1.000000000000000000, 0.000000000000000000, 0.000000000000000000 ) ) ;
#12117=B_SPLINE_CURVE_WITH_KNOTS ( 'NONE', 3,
 ( #2756, #8225, #12266, #21681, #2646, #1299, #12385, #19737 ),
 .UNSPECIFIED., .F., .F.,
 ( 4, 2, 2, 4 ),
 ( 0.003892319173193281752, 0.004864202078960306805, 0.005836084984727332725, 0.007779850796261384566 ),
 .UNSPECIFIED. ) ;
#12119=FACE_OUTER_BOUND ( 'NONE', #21618, .T. ) ;
#12126=CARTESIAN_POINT ( 'NONE',  ( 0.000000000000000000, -45.00000000000000000, 27.00000000000000000 ) ) ;
#12137=EDGE_CURVE ( 'NONE', #16240, #10789, #1701, .T. ) ;
#12153=CIRCLE ( 'NONE', #13712, 1.999999999999994449 ) ;
#12156=ORIENTED_EDGE ( 'NONE', *, *, #4500, .F. ) ;
#12168=ADVANCED_FACE ( 'NONE', ( #3107 ), #12482, .F. ) ;
#12179=VECTOR ( 'NONE', #17332, 1000.000000000000000 ) ;
#12180=DIRECTION ( 'NONE',  ( -1.000000000000000000, 0.000000000000000000, 0.000000000000000000 ) ) ;
#12182=VECTOR ( 'NONE', #1828, 1000.000000000000000 ) ;
#12192=CARTESIAN_POINT ( 'NONE',  ( 2.024999999999999911, -45.00000000000000000, -27.00000000000000000 ) ) ;
#12196=CIRCLE ( 'NONE', #15302, 15.00000000000000000 ) ;
#12198=ORIENTED_EDGE ( 'NONE', *, *, #3412, .F. ) ;
#12204=DIRECTION ( 'NONE',  ( 0.8571673007021116675, 0.000000000000000000, 0.5150380749100552658 ) ) ;
#12207=DIRECTION ( 'NONE',  ( -0.000000000000000000, -0.000000000000000000, 1.000000000000000000 ) ) ;
#12221=ORIENTED_EDGE ( 'NONE', *, *, #10179, .T. ) ;
#12223=EDGE_CURVE ( 'NONE', #7988, #18527, #1876, .T. ) ;
#12236=DIRECTION ( 'NONE',  ( 1.000000000000000000, 0.000000000000000000, 0.000000000000000000 ) ) ;
#12260=CYLINDRICAL_SURFACE ( 'NONE', #16473, 1.500000000000001332 ) ;
#12266=CARTESIAN_POINT ( 'NONE',  ( -14.98952570844870102, -0.6468970097546548059, 9.483487670324118213 ) ) ;
#12268=DIRECTION ( 'NONE',  ( -0.000000000000000000, -0.000000000000000000, -1.000000000000000000 ) ) ;
#12281=PRODUCT_DEFINITION ( 'UNKNOWN', '', #4562, #22878 ) ;
#12287=CARTESIAN_POINT ( 'NONE',  ( 29.00000000000000355, 29.50000000000000000, 27.00000000000000000 ) ) ;
#12315=DIRECTION ( 'NONE',  ( -1.000000000000000000, 0.000000000000000000, 0.000000000000000000 ) ) ;
#12317=VECTOR ( 'NONE', #7030, 1000.000000000000000 ) ;
#12319=VERTEX_POINT ( 'NONE', #22609 ) ;
#12320=VECTOR ( 'NONE', #5779, 1000.000000000000000 ) ;
#12324=FACE_OUTER_BOUND ( 'NONE', #9815, .T. ) ;
#12330=EDGE_LOOP ( 'NONE', ( #17115, #308, #682, #7453 ) ) ;
#12331=CARTESIAN_POINT ( 'NONE',  ( -14.67187117805616481, 3.178673068337430241, 8.975236025575924259 ) ) ;
#12339=DIRECTION ( 'NONE',  ( -0.000000000000000000, -0.000000000000000000, -1.000000000000000000 ) ) ;
#12348=EDGE_CURVE ( 'NONE', #11886, #2809, #17657, .T. ) ;
#12355=DIRECTION ( 'NONE',  ( 0.000000000000000000, 0.000000000000000000, 1.000000000000000000 ) ) ;
#12357=CARTESIAN_POINT ( 'NONE',  ( 0.000000000000000000, 0.000000000000000000, -27.00000000000000000 ) ) ;
#12363=FACE_OUTER_BOUND ( 'NONE', #12411, .T. ) ;
#12365=ORIENTED_EDGE ( 'NONE', *, *, #10596, .F. ) ;
#12369=LINE ( 'NONE', #10421, #5329 ) ;
#12374=CARTESIAN_POINT ( 'NONE',  ( -17.19784311473119587, -8.411123426659422364, 4.422670359120423278 ) ) ;
#12382=FACE_OUTER_BOUND ( 'NONE', #11354, .T. ) ;
#12383=DIRECTION ( 'NONE',  ( 1.000000000000000000, 0.000000000000000000, 0.000000000000000000 ) ) ;
#12385=CARTESIAN_POINT ( 'NONE',  ( -14.67173559926287396, -3.179195828807837909, 8.975010320294696697 ) ) ;
#12397=EDGE_LOOP ( 'NONE', ( #918, #23629, #22857 ) ) ;
#12405=CARTESIAN_POINT ( 'NONE',  ( -23.85000000000000497, 15.03999999999999915, -25.00000000000000000 ) ) ;
#12410=LINE ( 'NONE', #10914, #23078 ) ;
#12411=EDGE_LOOP ( 'NONE', ( #6855, #22451, #7585, #18630 ) ) ;
#12412=CARTESIAN_POINT ( 'NONE',  ( 0.000000000000000000, 45.00000000000000000, -27.00000000000000000 ) ) ;
#12414=CARTESIAN_POINT ( 'NONE',  ( 16.99687406587156957, 7.923972684219727114, 5.245599057861377368 ) ) ;
#12415=FACE_OUTER_BOUND ( 'NONE', #14755, .T. ) ;
#12431=ORIENTED_EDGE ( 'NONE', *, *, #23666, .F. ) ;
#12443=VECTOR ( 'NONE', #23392, 1000.000000000000000 ) ;
#12449=LINE ( 'NONE', #19913, #14946 ) ;
#12457=CARTESIAN_POINT ( 'NONE',  ( 28.27483331787888332, -41.23752903419610050, -27.00000000000000000 ) ) ;
#12478=ORIENTED_EDGE ( 'NONE', *, *, #22469, .F. ) ;
#12482=CYLINDRICAL_SURFACE ( 'NONE', #9447, 4.999999999999997335 ) ;
#12487=CARTESIAN_POINT ( 'NONE',  ( 0.000000000000000000, 45.00000000000000000, 23.99999999999999645 ) ) ;
#12489=FACE_OUTER_BOUND ( 'NONE', #5278, .T. ) ;
#12492=CARTESIAN_POINT ( 'NONE',  ( 0.000000000000000000, 45.00000000000000000, 23.99999999999999645 ) ) ;
#12494=EDGE_CURVE ( 'NONE', #5306, #5307, #6524, .T. ) ;
#12499=DIRECTION ( 'NONE',  ( 0.000000000000000000, 0.000000000000000000, 1.000000000000000000 ) ) ;
#12507=CARTESIAN_POINT ( 'NONE',  ( 0.000000000000000000, -15.23000000000000220, 27.00000000000000000 ) ) ;
#12512=LINE ( 'NONE', #20227, #14487 ) ;
#12516=CARTESIAN_POINT ( 'NONE',  ( 14.51962751333974389, 3.765689428759029234, 8.721787840009197268 ) ) ;
#12529=CARTESIAN_POINT ( 'NONE',  ( 40.00000000000000000, -29.50000000000000000, 27.00000000000000000 ) ) ;
#12530=ORIENTED_EDGE ( 'NONE', *, *, #6889, .F. ) ;
#12554=ORIENTED_EDGE ( 'NONE', *, *, #22501, .T. ) ;
#12556=DIRECTION ( 'NONE',  ( -0.000000000000000000, -0.000000000000000000, -1.000000000000000000 ) ) ;
#12558=CIRCLE ( 'NONE', #15680, 2.024999999999999911 ) ;
#12568=ORIENTED_EDGE ( 'NONE', *, *, #4568, .F. ) ;
#12570=DIRECTION ( 'NONE',  ( 0.000000000000000000, 0.000000000000000000, 1.000000000000000000 ) ) ;
#12588=CARTESIAN_POINT ( 'NONE',  ( 14.91530227160598798, -1.623290104782664445, 9.365835742197226921 ) ) ;
#12589=ORIENTED_EDGE ( 'NONE', *, *, #11974, .F. ) ;
#12592=LINE ( 'NONE', #16019, #107 ) ;
#12600=CIRCLE ( 'NONE', #15661, 1.999999999999994449 ) ;
#12601=ORIENTED_EDGE ( 'NONE', *, *, #19302, .F. ) ;
#12605=CARTESIAN_POINT ( 'NONE',  ( 0.000000000000000000, 15.23000000000000220, -27.00000000000000000 ) ) ;
#12617=DIRECTION ( 'NONE',  ( -1.000000000000000000, 0.000000000000000000, 0.000000000000000000 ) ) ;
#12625=CARTESIAN_POINT ( 'NONE',  ( 2.024999999999999911, 45.00000000000000000, -27.00000000000000000 ) ) ;
#12644=DIRECTION ( 'NONE',  ( -0.000000000000000000, -0.000000000000000000, 1.000000000000000000 ) ) ;
#12651=CARTESIAN_POINT ( 'NONE',  ( 17.32141611691247718, 8.728455122802976973, 3.780491077225283103 ) ) ;
#12672=DIRECTION ( 'NONE',  ( -0.000000000000000000, -0.000000000000000000, 1.000000000000000000 ) ) ;
#12676=EDGE_CURVE ( 'NONE', #13598, #11604, #21529, .T. ) ;
#12682=CARTESIAN_POINT ( 'NONE',  ( -34.10000000000000142, 29.50000000000000000, -27.00000000000000000 ) ) ;
#12685=CARTESIAN_POINT ( 'NONE',  ( -14.94708199919714176, 1.300481340138139430, 9.416259293296523225 ) ) ;
#12686=VECTOR ( 'NONE', #5323, 1000.000000000000000 ) ;
#12687=VERTEX_POINT ( 'NONE', #16142 ) ;
#12692=ORIENTED_EDGE ( 'NONE', *, *, #4568, .T. ) ;
#12702=EDGE_CURVE ( 'NONE', #3850, #2350, #5208, .T. ) ;
#12704=EDGE_CURVE ( 'NONE', #19865, #15990, #7518, .T. ) ;
#12707=ORIENTED_EDGE ( 'NONE', *, *, #2688, .T. ) ;
#12708=ORIENTED_EDGE ( 'NONE', *, *, #14810, .T. ) ;
#12710=CYLINDRICAL_SURFACE ( 'NONE', #3426, 10.99999999999999645 ) ;
#12715=CARTESIAN_POINT ( 'NONE',  ( 15.00000000000000178, -0.3242076166095157475, 9.499999999999987566 ) ) ;
#12727=ORIENTED_EDGE ( 'NONE', *, *, #3647, .T. ) ;
#12735=ORIENTED_EDGE ( 'NONE', *, *, #14379, .F. ) ;
#12737=CARTESIAN_POINT ( 'NONE',  ( -23.89999999999999858, 29.50000000000000000, 27.00000000000000000 ) ) ;
#12742=CARTESIAN_POINT ( 'NONE',  ( 2.024999999999999911, 45.00000000000000000, -27.00000000000000000 ) ) ;
#12768=ORIENTED_EDGE ( 'NONE', *, *, #4575, .T. ) ;
#12769=DIRECTION ( 'NONE',  ( -0.000000000000000000, -0.000000000000000000, 1.000000000000000000 ) ) ;
#12776=ORIENTED_EDGE ( 'NONE', *, *, #19488, .F. ) ;
#12777=EDGE_CURVE ( 'NONE', #5416, #7845, #22849, .T. ) ;
#12798=CARTESIAN_POINT ( 'NONE',  ( 18.49999999999999645, -15.23000000000000043, 27.00000000000000000 ) ) ;
#12799=CARTESIAN_POINT ( 'NONE',  ( -28.99999999999999645, 29.50000000000000000, -27.00000000000000000 ) ) ;
#12806=ORIENTED_EDGE ( 'NONE', *, *, #12137, .T. ) ;
#12809=ORIENTED_EDGE ( 'NONE', *, *, #9088, .T. ) ;
#12813=DIRECTION ( 'NONE',  ( -0.000000000000000000, -0.000000000000000000, 1.000000000000000000 ) ) ;
#12822=FACE_OUTER_BOUND ( 'NONE', #6211, .T. ) ;
#12831=DIRECTION ( 'NONE',  ( -0.000000000000000000, -0.000000000000000000, -1.000000000000000000 ) ) ;
#12842=ORIENTED_EDGE ( 'NONE', *, *, #21704, .F. ) ;
#12843=ORIENTED_EDGE ( 'NONE', *, *, #12777, .F. ) ;
#12873=CARTESIAN_POINT ( 'NONE',  ( 31.10231664966676135, 45.36128193761570770, 27.00000000000000000 ) ) ;
#12875=CARTESIAN_POINT ( 'NONE',  ( 41.99999999999999289, 25.93535998569253920, 27.00000000000000000 ) ) ;
#12876=EDGE_CURVE ( 'NONE', #4529, #6633, #7920, .T. ) ;
#12890=VERTEX_POINT ( 'NONE', #8166 ) ;
#12895=ORIENTED_EDGE ( 'NONE', *, *, #5723, .T. ) ;
#12907=( NAMED_UNIT ( * ) PLANE_ANGLE_UNIT ( ) SI_UNIT ( $, .RADIAN. ) );
#12908=VECTOR ( 'NONE', #19481, 1000.000000000000000 ) ;
#12929=VECTOR ( 'NONE', #23437, 1000.000000000000114 ) ;
#12945=FACE_OUTER_BOUND ( 'NONE', #22872, .T. ) ;
#12955=ORIENTED_EDGE ( 'NONE', *, *, #9611, .F. ) ;
#12960=ADVANCED_FACE ( 'NONE', ( #17458 ), #16951, .F. ) ;
#12964=AXIS2_PLACEMENT_3D ( 'NONE', #3790, #20621, #18671 ) ;
#12967=VECTOR ( 'NONE', #9470, 1000.000000000000114 ) ;
#12973=CARTESIAN_POINT ( 'NONE',  ( 20.85000000000000853, 15.03999999999999915, -27.00000000000000000 ) ) ;
#12975=MECHANICAL_DESIGN_GEOMETRIC_PRESENTATION_REPRESENTATION('',(#5989),#11801);
#12978=AXIS2_PLACEMENT_3D ( 'NONE', #7500, #22650, #9334 ) ;
#12981=AXIS2_PLACEMENT_3D ( 'NONE', #8080, #21289, #22750 ) ;
#12983=VERTEX_POINT ( 'NONE', #23075 ) ;
#13000=DIRECTION ( 'NONE',  ( 1.000000000000000000, -0.000000000000000000, -0.000000000000000000 ) ) ;
#13001=VERTEX_POINT ( 'NONE', #6969 ) ;
#13002=PLANE ( 'NONE',  #10606 ) ;
#13010=CARTESIAN_POINT ( 'NONE',  ( 15.56475192642548322, 5.220978644676159242, -7.947934502462939754 ) ) ;
#13022=EDGE_CURVE ( 'NONE', #23407, #12319, #18919, .T. ) ;
#13033=CARTESIAN_POINT ( 'NONE',  ( -17.59041996266972774, 9.500503876990130436, 0.4759723220310715375 ) ) ;
#13039=VECTOR ( 'NONE', #13761, 1000.000000000000000 ) ;
#13044=ORIENTED_EDGE ( 'NONE', *, *, #13561, .T. ) ;
#13054=DIRECTION ( 'NONE',  ( 1.000000000000000000, 0.000000000000000000, -0.000000000000000000 ) ) ;
#13056=EDGE_CURVE ( 'NONE', #7931, #5307, #14211, .T. ) ;
#13058=DIRECTION ( 'NONE',  ( -0.000000000000000000, -0.000000000000000000, -1.000000000000000000 ) ) ;
#13062=LINE ( 'NONE', #7434, #13039 ) ;
#13067=ORIENTED_EDGE ( 'NONE', *, *, #4266, .T. ) ;
#13088=EDGE_CURVE ( 'NONE', #13963, #11994, #9013, .T. ) ;
#13102=ORIENTED_EDGE ( 'NONE', *, *, #20639, .F. ) ;
#13110=EDGE_CURVE ( 'NONE', #12890, #732, #10491, .T. ) ;
#13111=CIRCLE ( 'NONE', #18192, 1.999999999999994449 ) ;
#13129=CARTESIAN_POINT ( 'NONE',  ( 0.000000000000000000, -45.00000000000000000, -26.97499999999999432 ) ) ;
#13133=DIRECTION ( 'NONE',  ( -0.8571673007021116675, 1.049727191138617833E-16, 0.5150380749100552658 ) ) ;
#13135=ORIENTED_EDGE ( 'NONE', *, *, #7733, .F. ) ;
#13137=EDGE_CURVE ( 'NONE', #12890, #13474, #20485, .T. ) ;
#13145=ORIENTED_EDGE ( 'NONE', *, *, #8354, .T. ) ;
#13166=PLANE ( 'NONE',  #4112 ) ;
#13176=DIRECTION ( 'NONE',  ( -0.000000000000000000, -0.000000000000000000, -1.000000000000000000 ) ) ;
#13177=CARTESIAN_POINT ( 'NONE',  ( 15.00000000000000178, 0.3242076166095267942, -9.499999999999987566 ) ) ;
#13192=CARTESIAN_POINT ( 'NONE',  ( 40.89823313241237912, 26.41789760203348081, -27.00000000000000000 ) ) ;
#13196=ORIENTED_EDGE ( 'NONE', *, *, #2494, .F. ) ;
#13200=CIRCLE ( 'NONE', #2701, 15.00000000000000000 ) ;
#13204=FACE_OUTER_BOUND ( 'NONE', #17975, .T. ) ;
#13220=AXIS2_PLACEMENT_3D ( 'NONE', #6802, #1193, #1446 ) ;
#13233=DIRECTION ( 'NONE',  ( -0.000000000000000000, -0.000000000000000000, -1.000000000000000000 ) ) ;
#13234=DIRECTION ( 'NONE',  ( 0.000000000000000000, 0.000000000000000000, 1.000000000000000000 ) ) ;
#13241=LINE ( 'NONE', #20696, #1608 ) ;
#13253=ORIENTED_EDGE ( 'NONE', *, *, #5926, .T. ) ;
#13257=DIRECTION ( 'NONE',  ( -1.000000000000000000, 0.000000000000000000, 0.000000000000000000 ) ) ;
#13262=CARTESIAN_POINT ( 'NONE',  ( -14.99999999999999822, 6.045577542124163753E-21, -9.499999999999994671 ) ) ;
#13265=DIRECTION ( 'NONE',  ( 1.000000000000000000, 0.000000000000000000, 0.000000000000000000 ) ) ;
#13272=AXIS2_PLACEMENT_3D ( 'NONE', #12492, #6430, #12383 ) ;
#13278=EDGE_LOOP ( 'NONE', ( #21950, #22459, #21777, #17927 ) ) ;
#13281=FACE_OUTER_BOUND ( 'NONE', #1830, .T. ) ;
#13287=ORIENTED_EDGE ( 'NONE', *, *, #6889, .T. ) ;
#13298=LINE ( 'NONE', #7230, #11401 ) ;
#13302=FACE_OUTER_BOUND ( 'NONE', #8883, .T. ) ;
#13306=CARTESIAN_POINT ( 'NONE',  ( -39.99999999999999289, -27.79189783386527779, 27.00000000000000000 ) ) ;
#13313=CYLINDRICAL_SURFACE ( 'NONE', #2946, 14.99999999999999822 ) ;
#13317=AXIS2_PLACEMENT_3D ( 'NONE', #3977, #11396, #11530 ) ;
#13340=ORIENTED_EDGE ( 'NONE', *, *, #688, .T. ) ;
#13345=AXIS2_PLACEMENT_3D ( 'NONE', #5889, #409, #13458 ) ;
#13350=ORIENTED_EDGE ( 'NONE', *, *, #3675, .F. ) ;
#13358=DIRECTION ( 'NONE',  ( -1.000000000000000000, 0.000000000000000000, 0.000000000000000000 ) ) ;
#13363=EDGE_CURVE ( 'NONE', #4173, #19649, #14806, .T. ) ;
#13364=CARTESIAN_POINT ( 'NONE',  ( 29.00000000000000711, -29.50000000000000711, 27.00000000000000000 ) ) ;
#13369=DIRECTION ( 'NONE',  ( -0.000000000000000000, -0.000000000000000000, -1.000000000000000000 ) ) ;
#13386=FACE_OUTER_BOUND ( 'NONE', #15286, .T. ) ;
#13393=AXIS2_PLACEMENT_3D ( 'NONE', #6292, #13738, #4976 ) ;
#13400=CARTESIAN_POINT ( 'NONE',  ( -20.85000000000000853, 15.04000000000000092, -25.00000000000000000 ) ) ;
#13404=CIRCLE ( 'NONE', #2902, 1.999999999999994449 ) ;
#13409=EDGE_CURVE ( 'NONE', #9227, #5616, #16250, .T. ) ;
#13412=DIRECTION ( 'NONE',  ( 1.000000000000000000, 0.000000000000000000, 0.000000000000000000 ) ) ;
#13419=EDGE_CURVE ( 'NONE', #2676, #18226, #22044, .T. ) ;
#13420=CARTESIAN_POINT ( 'NONE',  ( 14.94777716362147935, -1.291632522116889170, -9.417361603030268924 ) ) ;
#13436=DIRECTION ( 'NONE',  ( 0.000000000000000000, 0.000000000000000000, 1.000000000000000000 ) ) ;
#13440=DIRECTION ( 'NONE',  ( -0.000000000000000000, -0.000000000000000000, -1.000000000000000000 ) ) ;
#13445=CARTESIAN_POINT ( 'NONE',  ( 2.024999999999999911, -45.00000000000000000, 27.00000000000000000 ) ) ;
#13450=AXIS2_PLACEMENT_3D ( 'NONE', #14402, #12813, #8801 ) ;
#13451=VERTEX_POINT ( 'NONE', #22624 ) ;
#13453=VECTOR ( 'NONE', #15592, 1000.000000000000114 ) ;
#13458=DIRECTION ( 'NONE',  ( 0.000000000000000000, 0.000000000000000000, 1.000000000000000000 ) ) ;
#13469=CARTESIAN_POINT ( 'NONE',  ( -2.024999999999999911, -45.00000000000000000, 27.00000000000000000 ) ) ;
#13474=VERTEX_POINT ( 'NONE', #9669 ) ;
#13494=FACE_OUTER_BOUND ( 'NONE', #4860, .T. ) ;
#13496=DIRECTION ( 'NONE',  ( -0.000000000000000000, -0.000000000000000000, 1.000000000000000000 ) ) ;
#13502=CARTESIAN_POINT ( 'NONE',  ( -30.44534269664590198, 40.40463133211079594, 27.00000000000000000 ) ) ;
#13504=CARTESIAN_POINT ( 'NONE',  ( -23.85000000000000497, 15.03999999999999915, 25.00000000000000000 ) ) ;
#13506=CARTESIAN_POINT ( 'NONE',  ( -1.999999999999994449, -45.00000000000000000, 23.99999999999999645 ) ) ;
#13507=DIRECTION ( 'NONE',  ( -1.000000000000000000, 0.000000000000000000, 0.000000000000000000 ) ) ;
#13530=ORIENTED_EDGE ( 'NONE', *, *, #23641, .T. ) ;
#13533=CARTESIAN_POINT ( 'NONE',  ( 0.000000000000000000, 15.03999999999999915, -25.00000000000000000 ) ) ;
#13536=ORIENTED_EDGE ( 'NONE', *, *, #2463, .F. ) ;
#13548=VERTEX_POINT ( 'NONE', #8468 ) ;
#13553=ORIENTED_EDGE ( 'NONE', *, *, #15735, .T. ) ;
#13555=EDGE_CURVE ( 'NONE', #11452, #15990, #1161, .T. ) ;
#13561=EDGE_CURVE ( 'NONE', #19529, #16240, #21291, .T. ) ;
#13564=CARTESIAN_POINT ( 'NONE',  ( 1.999999999999994449, 45.00000000000000000, 27.00000000000000000 ) ) ;
#13570=EDGE_CURVE ( 'NONE', #23352, #22892, #1798, .T. ) ;
#13575=AXIS2_PLACEMENT_3D ( 'NONE', #6229, #15372, #6117 ) ;
#13576=ORIENTED_EDGE ( 'NONE', *, *, #16470, .T. ) ;
#13598=VERTEX_POINT ( 'NONE', #8199 ) ;
#13619=CIRCLE ( 'NONE', #17124, 18.49999999999999645 ) ;
#13635=ORIENTED_EDGE ( 'NONE', *, *, #4262, .T. ) ;
#13643=DIRECTION ( 'NONE',  ( 0.000000000000000000, 0.000000000000000000, 1.000000000000000000 ) ) ;
#13655=ORIENTED_EDGE ( 'NONE', *, *, #8439, .T. ) ;
#13664=VERTEX_POINT ( 'NONE', #5293 ) ;
#13677=ORIENTED_EDGE ( 'NONE', *, *, #17495, .T. ) ;
#13687=DIRECTION ( 'NONE',  ( -0.000000000000000000, -0.000000000000000000, -1.000000000000000000 ) ) ;
#13688=VERTEX_POINT ( 'NONE', #23723 ) ;
#13696=VERTEX_POINT ( 'NONE', #1518 ) ;
#13699=VECTOR ( 'NONE', #20083, 1000.000000000000000 ) ;
#13705=ORIENTED_EDGE ( 'NONE', *, *, #186, .T. ) ;
#13706=ORIENTED_EDGE ( 'NONE', *, *, #20845, .T. ) ;
#13712=AXIS2_PLACEMENT_3D ( 'NONE', #13129, #13369, #20831 ) ;
#13725=CARTESIAN_POINT ( 'NONE',  ( 0.000000000000000000, 45.00000000000000000, 26.97499999999999432 ) ) ;
#13738=DIRECTION ( 'NONE',  ( 0.000000000000000000, 0.000000000000000000, 1.000000000000000000 ) ) ;
#13745=ORIENTED_EDGE ( 'NONE', *, *, #12494, .F. ) ;
#13760=ORIENTED_EDGE ( 'NONE', *, *, #6830, .T. ) ;
#13761=DIRECTION ( 'NONE',  ( -0.000000000000000000, -0.000000000000000000, -1.000000000000000000 ) ) ;
#13782=EDGE_CURVE ( 'NONE', #23345, #17607, #2225, .T. ) ;
#13784=AXIS2_PLACEMENT_3D ( 'NONE', #12605, #20072, #16716 ) ;
#13794=ORIENTED_EDGE ( 'NONE', *, *, #5926, .F. ) ;
#13795=DIRECTION ( 'NONE',  ( 0.000000000000000000, 0.000000000000000000, 1.000000000000000000 ) ) ;
#13803=AXIS2_PLACEMENT_3D ( 'NONE', #2872, #4964, #10424 ) ;
#13809=AXIS2_PLACEMENT_3D ( 'NONE', #6326, #14018, #2557 ) ;
#13818=ORIENTED_EDGE ( 'NONE', *, *, #22390, .T. ) ;
#13831=VERTEX_POINT ( 'NONE', #5133 ) ;
#13835=DIRECTION ( 'NONE',  ( 0.000000000000000000, 0.000000000000000000, 1.000000000000000000 ) ) ;
#13845=ORIENTED_EDGE ( 'NONE', *, *, #18920, .T. ) ;
#13847=EDGE_LOOP ( 'NONE', ( #15343, #20813, #20608, #14462, #16623, #17089, #4358, #11750, #17293, #15561, #4916, #15391, #23471, #8647, #15918, #10950, #1891, #18978, #11480, #2264, #8888, #1128, #11651, #17243 ) ) ;
#13850=ORIENTED_EDGE ( 'NONE', *, *, #15885, .T. ) ;
#13860=CARTESIAN_POINT ( 'NONE',  ( -14.67187117805616126, -3.178673068337432461, -8.975236025575920706 ) ) ;
#13862=CARTESIAN_POINT ( 'NONE',  ( -15.57833309066360350, -5.219313726039664481, 7.987432870209368652 ) ) ;
#13867=ORIENTED_EDGE ( 'NONE', *, *, #5723, .F. ) ;
#13874=CARTESIAN_POINT ( 'NONE',  ( 16.68233279685676251, -7.225448002938847480, -6.184784653374910235 ) ) ;
#13884=ADVANCED_FACE ( 'NONE', ( #14259 ), #9578, .F. ) ;
#13889=AXIS2_PLACEMENT_3D ( 'NONE', #11656, #4509, #19625 ) ;
#13892=LINE ( 'NONE', #15834, #6885 ) ;
#13893=CARTESIAN_POINT ( 'NONE',  ( -28.99999999999999645, 29.50000000000000000, -27.00000000000000000 ) ) ;
#13897=DIRECTION ( 'NONE',  ( -0.000000000000000000, -0.000000000000000000, 1.000000000000000000 ) ) ;
#13899=EDGE_CURVE ( 'NONE', #22869, #3165, #16323, .T. ) ;
#13903=LINE ( 'NONE', #21346, #16857 ) ;
#13923=DIRECTION ( 'NONE',  ( -1.337728473353585242E-16, 1.000000000000000000, -0.000000000000000000 ) ) ;
#13931=EDGE_CURVE ( 'NONE', #22311, #15047, #11526, .T. ) ;
#13939=CARTESIAN_POINT ( 'NONE',  ( -20.85000000000000853, 15.04000000000000092, 25.00000000000000000 ) ) ;
#13943=CARTESIAN_POINT ( 'NONE',  ( 34.10000000000000853, 29.50000000000000000, 27.00000000000000000 ) ) ;
#13951=ORIENTED_EDGE ( 'NONE', *, *, #6251, .F. ) ;
#13963=VERTEX_POINT ( 'NONE', #23223 ) ;
#13966=DIRECTION ( 'NONE',  ( 0.000000000000000000, 0.000000000000000000, 1.000000000000000000 ) ) ;
#13971=ORIENTED_EDGE ( 'NONE', *, *, #13409, .F. ) ;
#13972=VERTEX_POINT ( 'NONE', #12077 ) ;
#13979=CARTESIAN_POINT ( 'NONE',  ( -17.59008829125738060, -9.499485695642615468, 0.4958780962348248722 ) ) ;
#13984=DIRECTION ( 'NONE',  ( -0.000000000000000000, -0.000000000000000000, -1.000000000000000000 ) ) ;
#13985=EDGE_CURVE ( 'NONE', #14530, #23937, #11313, .T. ) ;
#14012=ORIENTED_EDGE ( 'NONE', *, *, #14215, .T. ) ;
#14018=DIRECTION ( 'NONE',  ( -0.000000000000000000, -0.000000000000000000, -1.000000000000000000 ) ) ;
#14026=CIRCLE ( 'NONE', #13220, 14.99999999999999822 ) ;
#14041=LINE ( 'NONE', #12192, #16405 ) ;
#14058=ORIENTED_EDGE ( 'NONE', *, *, #18494, .T. ) ;
#14060=EDGE_CURVE ( 'NONE', #18444, #13696, #14674, .T. ) ;
#14063=ORIENTED_EDGE ( 'NONE', *, *, #22469, .T. ) ;
#14088=CARTESIAN_POINT ( 'NONE',  ( 40.00000000000000711, 29.50000000000000000, -27.00000000000000000 ) ) ;
#14104=ORIENTED_EDGE ( 'NONE', *, *, #1640, .F. ) ;
#14111=ORIENTED_EDGE ( 'NONE', *, *, #12106, .T. ) ;
#14129=AXIS2_PLACEMENT_3D ( 'NONE', #2355, #19082, #7955 ) ;
#14133=EDGE_LOOP ( 'NONE', ( #826, #14063, #5524, #5249 ) ) ;
#14138=DIRECTION ( 'NONE',  ( -1.000000000000000000, 0.000000000000000000, 0.000000000000000000 ) ) ;
#14153=( LENGTH_UNIT ( ) NAMED_UNIT ( * ) SI_UNIT ( .MILLI., .METRE. ) );
#14159=AXIS2_PLACEMENT_3D ( 'NONE', #5405, #9169, #23605 ) ;
#14165=AXIS2_PLACEMENT_3D ( 'NONE', #14780, #22134, #11326 ) ;
#14168=FACE_BOUND ( 'NONE', #11610, .T. ) ;
#14169=ADVANCED_FACE ( 'NONE', ( #21473 ), #14622, .F. ) ;
#14171=EDGE_CURVE ( 'NONE', #21663, #5301, #10099, .T. ) ;
#14199=CARTESIAN_POINT ( 'NONE',  ( 0.000000000000000000, 0.000000000000000000, 27.00000000000000000 ) ) ;
#14202=CARTESIAN_POINT ( 'NONE',  ( -16.82499651802897489, -7.532250541895351148, -5.808290850931487448 ) ) ;
#14206=CARTESIAN_POINT ( 'NONE',  ( 0.000000000000000000, -45.00000000000000000, -26.97499999999999432 ) ) ;
#14207=VECTOR ( 'NONE', #21237, 1000.000000000000000 ) ;
#14211=B_SPLINE_CURVE_WITH_KNOTS ( 'NONE', 3,
 ( #1371, #12331, #16590, #23800, #12685, #7199, #21741, #5031 ),
 .UNSPECIFIED., .F., .F.,
 ( 4, 2, 2, 4 ),
 ( 2.602085213965210256E-18, 0.001946159586596642611, 0.002919239379894961964, 0.003892319173193281752 ),
 .UNSPECIFIED. ) ;
#14212=CARTESIAN_POINT ( 'NONE',  ( -39.99999999999999289, -29.50000000000001066, -27.00000000000000000 ) ) ;
#14213=CARTESIAN_POINT ( 'NONE',  ( -20.85000000000000853, 15.04000000000000092, -25.00000000000000000 ) ) ;
#14215=EDGE_CURVE ( 'NONE', #23407, #23565, #2931, .T. ) ;
#14216=CARTESIAN_POINT ( 'NONE',  ( 17.49232137458054837, -9.205685982891273156, 2.395442301836270715 ) ) ;
#14222=AXIS2_PLACEMENT_3D ( 'NONE', #23029, #15322, #4508 ) ;
#14229=EDGE_LOOP ( 'NONE', ( #5412, #709, #15756 ) ) ;
#14244=VERTEX_POINT ( 'NONE', #15973 ) ;
#14247=ADVANCED_FACE ( 'NONE', ( #23432 ), #21723, .F. ) ;
#14259=FACE_OUTER_BOUND ( 'NONE', #16674, .T. ) ;
#14263=VECTOR ( 'NONE', #17985, 1000.000000000000000 ) ;
#14266=CARTESIAN_POINT ( 'NONE',  ( 40.99749999999998096, 5.618459588085056979E-15, -9.499999999999989342 ) ) ;
#14269=AXIS2_PLACEMENT_3D ( 'NONE', #21453, #4745, #9959 ) ;
#14276=PLANE ( 'NONE',  #7516 ) ;
#14279=DIRECTION ( 'NONE',  ( -0.000000000000000000, -0.000000000000000000, -1.000000000000000000 ) ) ;
#14288=ORIENTED_EDGE ( 'NONE', *, *, #14442, .T. ) ;
#14289=LINE ( 'NONE', #21984, #6515 ) ;
#14312=ORIENTED_EDGE ( 'NONE', *, *, #22907, .T. ) ;
#14322=LINE ( 'NONE', #8944, #18979 ) ;
#14328=DIRECTION ( 'NONE',  ( -0.000000000000000000, -0.000000000000000000, -1.000000000000000000 ) ) ;
#14330=AXIS2_PLACEMENT_3D ( 'NONE', #12873, #3385, #5452 ) ;
#14332=CARTESIAN_POINT ( 'NONE',  ( 17.32314925601268740, -8.733074366907743524, 3.769949228126185048 ) ) ;
#14339=AXIS2_PLACEMENT_3D ( 'NONE', #15259, #410, #7460 ) ;
#14342=ORIENTED_EDGE ( 'NONE', *, *, #6603, .F. ) ;
#14343=EDGE_LOOP ( 'NONE', ( #19445, #17363 ) ) ;
#14344=FACE_OUTER_BOUND ( 'NONE', #3863, .T. ) ;
#14349=CYLINDRICAL_SURFACE ( 'NONE', #2158, 18.49999999999999645 ) ;
#14371=DIRECTION ( 'NONE',  ( 1.000000000000000000, -0.000000000000000000, -0.000000000000000000 ) ) ;
#14375=CYLINDRICAL_SURFACE ( 'NONE', #7060, 9.499999999999994671 ) ;
#14379=EDGE_CURVE ( 'NONE', #5307, #21442, #12117, .T. ) ;
#14395=ORIENTED_EDGE ( 'NONE', *, *, #19579, .T. ) ;
#14399=DIRECTION ( 'NONE',  ( -1.000000000000000000, 0.000000000000000000, 0.000000000000000000 ) ) ;
#14401=CYLINDRICAL_SURFACE ( 'NONE', #1657, 1.999999999999994449 ) ;
#14402=CARTESIAN_POINT ( 'NONE',  ( 0.000000000000000000, -45.00000000000000000, 23.99999999999999645 ) ) ;
#14412=FACE_OUTER_BOUND ( 'NONE', #7722, .T. ) ;
#14418=CARTESIAN_POINT ( 'NONE',  ( -40.89823313241237912, 26.41789760203348081, 27.00000000000000000 ) ) ;
#14421=CIRCLE ( 'NONE', #8964, 4.999999999999997335 ) ;
#14438=DIRECTION ( 'NONE',  ( -0.000000000000000000, -0.000000000000000000, 1.000000000000000000 ) ) ;
#14442=EDGE_CURVE ( 'NONE', #23460, #13598, #6618, .T. ) ;
#14452=EDGE_LOOP ( 'NONE', ( #20373, #969, #17247 ) ) ;
#14455=FACE_OUTER_BOUND ( 'NONE', #21230, .T. ) ;
#14462=ORIENTED_EDGE ( 'NONE', *, *, #11157, .F. ) ;
#14466=ORIENTED_EDGE ( 'NONE', *, *, #9930, .F. ) ;
#14487=VECTOR ( 'NONE', #16203, 1000.000000000000000 ) ;
#14492=PRODUCT_DEFINITION_SHAPE ( 'NONE', 'NONE',  #12281 ) ;
#14497=ORIENTED_EDGE ( 'NONE', *, *, #2494, .T. ) ;
#14507=VERTEX_POINT ( 'NONE', #12973 ) ;
#14508=CIRCLE ( 'NONE', #10223, 1.999999999999994449 ) ;
#14517=FACE_BOUND ( 'NONE', #2795, .T. ) ;
#14530=VERTEX_POINT ( 'NONE', #7362 ) ;
#14541=CARTESIAN_POINT ( 'NONE',  ( -40.99749999999999517, 0.000000000000000000, 0.000000000000000000 ) ) ;
#14546=ADVANCED_FACE ( 'NONE', ( #19110 ), #21179, .F. ) ;
#14548=EDGE_CURVE ( 'NONE', #20316, #18527, #19321, .T. ) ;
#14559=ORIENTED_EDGE ( 'NONE', *, *, #4655, .T. ) ;
#14569=CONICAL_SURFACE ( 'NONE', #20828, 1.999999999999994449, 1.029744258676653201 ) ;
#14594=ORIENTED_EDGE ( 'NONE', *, *, #10848, .T. ) ;
#14596=AXIS2_PLACEMENT_3D ( 'NONE', #15200, #21079, #17426 ) ;
#14599=FACE_OUTER_BOUND ( 'NONE', #17859, .T. ) ;
#14618=FACE_OUTER_BOUND ( 'NONE', #7753, .T. ) ;
#14621=LINE ( 'NONE', #15193, #9952 ) ;
#14622=CONICAL_SURFACE ( 'NONE', #11484, 2.024999999999999911, 0.7853981633974743692 ) ;
#14627=CARTESIAN_POINT ( 'NONE',  ( -30.44534269664590198, -40.40463133211081015, -27.00000000000000000 ) ) ;
#14640=VERTEX_POINT ( 'NONE', #16038 ) ;
#14649=CARTESIAN_POINT ( 'NONE',  ( -41.49999999999999289, 27.79189783386526358, 27.00000000000000000 ) ) ;
#14655=FACE_OUTER_BOUND ( 'NONE', #22851, .T. ) ;
#14665=ORIENTED_EDGE ( 'NONE', *, *, #13985, .F. ) ;
#14670=ORIENTED_EDGE ( 'NONE', *, *, #10438, .T. ) ;
#14674=CIRCLE ( 'NONE', #20872, 10.50249999999999950 ) ;
#14675=DIRECTION ( 'NONE',  ( -0.000000000000000000, -0.000000000000000000, -1.000000000000000000 ) ) ;
#14679=ORIENTED_EDGE ( 'NONE', *, *, #8800, .F. ) ;
#14682=ADVANCED_FACE ( 'NONE', ( #10428 ), #22444, .F. ) ;
#14687=EDGE_CURVE ( 'NONE', #9227, #7988, #19843, .T. ) ;
#14694=LINE ( 'NONE', #1290, #20830 ) ;
#14717=DIRECTION ( 'NONE',  ( 1.000000000000000000, 0.000000000000000000, 0.000000000000000000 ) ) ;
#14725=DIRECTION ( 'NONE',  ( -1.000000000000000000, 0.000000000000000000, 0.000000000000000000 ) ) ;
#14727=CARTESIAN_POINT ( 'NONE',  ( 16.44572538483723534, 6.755397553796131049, 6.683320200552552492 ) ) ;
#14728=CARTESIAN_POINT ( 'NONE',  ( 1.999999999999994449, 45.00000000000000000, -23.99999999999999645 ) ) ;
#14751=CARTESIAN_POINT ( 'NONE',  ( -34.10000000000000142, 29.50000000000000000, 27.00000000000000000 ) ) ;
#14755=EDGE_LOOP ( 'NONE', ( #19109, #11693, #2079, #20748 ) ) ;
#14761=VERTEX_POINT ( 'NONE', #18479 ) ;
#14779=CARTESIAN_POINT ( 'NONE',  ( 14.67187117805616303, -3.178673068337433349, 8.975236025575910048 ) ) ;
#14780=CARTESIAN_POINT ( 'NONE',  ( 0.000000000000000000, 0.000000000000000000, 27.00000000000000000 ) ) ;
#14791=VECTOR ( 'NONE', #21489, 1000.000000000000000 ) ;
#14806=LINE ( 'NONE', #12625, #21680 ) ;
#14810=EDGE_CURVE ( 'NONE', #20027, #4529, #4650, .T. ) ;
#14817=ORIENTED_EDGE ( 'NONE', *, *, #4120, .F. ) ;
#14819=CARTESIAN_POINT ( 'NONE',  ( -41.99999999999999289, 25.93535998569253920, -27.00000000000000000 ) ) ;
#14821=B_SPLINE_CURVE_WITH_KNOTS ( 'NONE', 3,
 ( #12000, #21544, #13862, #17621, #803, #6544, #6901, #4842, #17762, #15664, #1174, #19472, #12374, #8714, #8584, #23136, #6419, #16030, #13979, #4712, #21421, #21309, #4599, #17994, #23497, #2748, #6776, #14202, #19839, #10164, #16163, #928, #8352, #1529, #8942, #1764 ),
 .UNSPECIFIED., .F., .F.,
 ( 4, 2, 2, 2, 2, 2, 2, 2, 2, 2, 2, 2, 2, 2, 2, 2, 2, 4 ),
 ( 0.000000000000000000, 0.002901772246161908077, 0.003627215307702382711, 0.004352658369242857345, 0.005803544492323810949, 0.006528987553864288619, 0.007254430615404765421, 0.008705316738485725098, 0.01015620286156668217, 0.01160708898464764272, 0.01305797510772860326, 0.01450886123080956033, 0.01595974735389052088, 0.01741063347697148142, 0.01886151960005243849, 0.02031240572313339557, 0.02176329184621435611, 0.02321417796929531666 ),
 .UNSPECIFIED. ) ;
#14823=ORIENTED_EDGE ( 'NONE', *, *, #16679, .F. ) ;
#14830=DIRECTION ( 'NONE',  ( -1.000000000000000000, 0.000000000000000000, 0.000000000000000000 ) ) ;
#14835=VERTEX_POINT ( 'NONE', #14266 ) ;
#14856=CARTESIAN_POINT ( 'NONE',  ( 0.000000000000000000, -45.00000000000000000, -27.00000000000000000 ) ) ;
#14867=VECTOR ( 'NONE', #15334, 1000.000000000000000 ) ;
#14868=CIRCLE ( 'NONE', #23470, 1.999999999999994449 ) ;
#14873=AXIS2_PLACEMENT_3D ( 'NONE', #16846, #12831, #4057 ) ;
#14874=CARTESIAN_POINT ( 'NONE',  ( -1.999999999999994449, -45.00000000000000000, -27.00000000000000000 ) ) ;
#14904=CIRCLE ( 'NONE', #915, 1.999999999999994449 ) ;
#14915=ADVANCED_FACE ( 'NONE', ( #20482 ), #18652, .F. ) ;
#14925=ORIENTED_EDGE ( 'NONE', *, *, #10940, .F. ) ;
#14933=ORIENTED_EDGE ( 'NONE', *, *, #346, .F. ) ;
#14946=VECTOR ( 'NONE', #12339, 1000.000000000000000 ) ;
#14949=ADVANCED_FACE ( 'NONE', ( #11655 ), #3994, .F. ) ;
#14952=CARTESIAN_POINT ( 'NONE',  ( 29.00000000000000711, -29.50000000000000711, 27.00000000000000000 ) ) ;
#14966=ADVANCED_FACE ( 'NONE', ( #11413 ), #17339, .F. ) ;
#14973=CYLINDRICAL_SURFACE ( 'NONE', #16442, 5.100000000000000533 ) ;
#14977=EDGE_CURVE ( 'NONE', #21663, #18617, #4367, .T. ) ;
#14979=DIRECTION ( 'NONE',  ( -1.000000000000000000, 4.613626265895763066E-16, 0.000000000000000000 ) ) ;
#14987=CARTESIAN_POINT ( 'NONE',  ( -23.89999999999999858, -29.50000000000001066, -27.00000000000000000 ) ) ;
#14989=VERTEX_POINT ( 'NONE', #10192 ) ;
#14999=ORIENTED_EDGE ( 'NONE', *, *, #19550, .F. ) ;
#15007=CARTESIAN_POINT ( 'NONE',  ( 23.84999999999999432, -15.03999999999999559, -27.00000000000000000 ) ) ;
#15020=ORIENTED_EDGE ( 'NONE', *, *, #19171, .F. ) ;
#15023=VECTOR ( 'NONE', #372, 1000.000000000000000 ) ;
#15035=DIRECTION ( 'NONE',  ( 0.000000000000000000, 0.000000000000000000, 1.000000000000000000 ) ) ;
#15047=VERTEX_POINT ( 'NONE', #15833 ) ;
#15048=ORIENTED_EDGE ( 'NONE', *, *, #8144, .F. ) ;
#15055=ORIENTED_EDGE ( 'NONE', *, *, #15735, .F. ) ;
#15067=CARTESIAN_POINT ( 'NONE',  ( -34.10000000000000142, -29.50000000000001066, -27.00000000000000000 ) ) ;
#15077=VERTEX_POINT ( 'NONE', #8504 ) ;
#15082=CARTESIAN_POINT ( 'NONE',  ( 28.27483331787888332, -41.23752903419610050, 27.00000000000000000 ) ) ;
#15084=ADVANCED_FACE ( 'NONE', ( #954, #14344 ), #16059, .F. ) ;
#15085=CARTESIAN_POINT ( 'NONE',  ( 29.00000000000000355, 29.50000000000000000, 27.00000000000000000 ) ) ;
#15091=DIRECTION ( 'NONE',  ( -0.000000000000000000, -0.000000000000000000, -1.000000000000000000 ) ) ;
#15109=DIRECTION ( 'NONE',  ( 0.000000000000000000, -1.000000000000000000, 0.000000000000000000 ) ) ;
#15116=ORIENTED_EDGE ( 'NONE', *, *, #9451, .F. ) ;
#15120=DIRECTION ( 'NONE',  ( 0.000000000000000000, 0.000000000000000000, 1.000000000000000000 ) ) ;
#15135=EDGE_CURVE ( 'NONE', #17527, #22631, #18621, .T. ) ;
#15155=ORIENTED_EDGE ( 'NONE', *, *, #2483, .T. ) ;
#15172=DIRECTION ( 'NONE',  ( 0.000000000000000000, 0.000000000000000000, 1.000000000000000000 ) ) ;
#15173=CARTESIAN_POINT ( 'NONE',  ( -40.89823313241237912, 26.41789760203348081, 27.00000000000000000 ) ) ;
#15176=ORIENTED_EDGE ( 'NONE', *, *, #7703, .T. ) ;
#15182=ADVANCED_FACE ( 'NONE', ( #14455 ), #16762, .F. ) ;
#15183=DIRECTION ( 'NONE',  ( -0.7071067811865469066, 0.000000000000000000, 0.7071067811865482389 ) ) ;
#15193=CARTESIAN_POINT ( 'NONE',  ( -39.99999999999999289, -27.79189783386527779, 27.00000000000000000 ) ) ;
#15200=CARTESIAN_POINT ( 'NONE',  ( 0.000000000000000000, -15.23000000000000220, -27.00000000000000000 ) ) ;
#15201=EDGE_CURVE ( 'NONE', #18612, #23403, #79, .T. ) ;
#15221=CARTESIAN_POINT ( 'NONE',  ( 23.90000000000000924, -29.50000000000000711, 27.00000000000000000 ) ) ;
#15223=VECTOR ( 'NONE', #4609, 1000.000000000000000 ) ;
#15225=FACE_OUTER_BOUND ( 'NONE', #19697, .T. ) ;
#15227=CYLINDRICAL_SURFACE ( 'NONE', #19566, 18.49999999999999645 ) ;
#15228=ORIENTED_EDGE ( 'NONE', *, *, #21474, .F. ) ;
#15243=FACE_OUTER_BOUND ( 'NONE', #18317, .T. ) ;
#15259=CARTESIAN_POINT ( 'NONE',  ( -41.49999999999999289, 27.79189783386526358, 27.00000000000000000 ) ) ;
#15263=VECTOR ( 'NONE', #12207, 1000.000000000000000 ) ;
#15268=CYLINDRICAL_SURFACE ( 'NONE', #14129, 5.100000000000000533 ) ;
#15280=CIRCLE ( 'NONE', #9832, 11.00000000000000711 ) ;
#15286=EDGE_LOOP ( 'NONE', ( #21167, #8121, #11777, #18559 ) ) ;
#15288=LINE ( 'NONE', #6048, #9593 ) ;
#15296=DIRECTION ( 'NONE',  ( -0.000000000000000000, -0.000000000000000000, -1.000000000000000000 ) ) ;
#15301=DIRECTION ( 'NONE',  ( -0.000000000000000000, -0.000000000000000000, -1.000000000000000000 ) ) ;
#15302=AXIS2_PLACEMENT_3D ( 'NONE', #8841, #9509, #5182 ) ;
#15304=ORIENTED_EDGE ( 'NONE', *, *, #16535, .F. ) ;
#15308=CIRCLE ( 'NONE', #11786, 23.84999999999999432 ) ;
#15322=DIRECTION ( 'NONE',  ( -0.000000000000000000, -0.000000000000000000, 1.000000000000000000 ) ) ;
#15324=EDGE_CURVE ( 'NONE', #8771, #22613, #11776, .T. ) ;
#15327=DIRECTION ( 'NONE',  ( -0.000000000000000000, -0.000000000000000000, 1.000000000000000000 ) ) ;
#15334=DIRECTION ( 'NONE',  ( 4.613626265895764052E-16, -1.000000000000000000, 0.000000000000000000 ) ) ;
#15341=CARTESIAN_POINT ( 'NONE',  ( -16.08510323282435550, 6.088885580147183951, -7.295537496892093188 ) ) ;
#15343=ORIENTED_EDGE ( 'NONE', *, *, #7804, .F. ) ;
#15350=VECTOR ( 'NONE', #1030, 1000.000000000000114 ) ;
#15357=CARTESIAN_POINT ( 'NONE',  ( 0.000000000000000000, 15.03999999999999915, 27.00000000000000000 ) ) ;
#15368=ORIENTED_EDGE ( 'NONE', *, *, #15703, .F. ) ;
#15372=DIRECTION ( 'NONE',  ( -0.000000000000000000, 0.000000000000000000, -1.000000000000000000 ) ) ;
#15373=VECTOR ( 'NONE', #21963, 1000.000000000000000 ) ;
#15391=ORIENTED_EDGE ( 'NONE', *, *, #22501, .F. ) ;
#15392=DIRECTION ( 'NONE',  ( 0.000000000000000000, 0.000000000000000000, -1.000000000000000000 ) ) ;
#15408=AXIS2_PLACEMENT_3D ( 'NONE', #15085, #22550, #5830 ) ;
#15432=CARTESIAN_POINT ( 'NONE',  ( 0.000000000000000000, -15.23000000000000220, -27.00000000000000000 ) ) ;
#15433=DIRECTION ( 'NONE',  ( 0.8571673007021116675, 0.000000000000000000, 0.5150380749100552658 ) ) ;
#15435=DIRECTION ( 'NONE',  ( -1.000000000000000000, -4.613626265895764052E-16, 0.000000000000000000 ) ) ;
#15441=ORIENTED_EDGE ( 'NONE', *, *, #9930, .T. ) ;
#15442=LINE ( 'NONE', #11896, #12443 ) ;
#15454=CARTESIAN_POINT ( 'NONE',  ( 0.000000000000000000, 0.000000000000000000, -27.00000000000000000 ) ) ;
#15457=DIRECTION ( 'NONE',  ( 4.613626265895763066E-16, 1.000000000000000000, -0.000000000000000000 ) ) ;
#15465=DIRECTION ( 'NONE',  ( 0.000000000000000000, 1.000000000000000000, 0.000000000000000000 ) ) ;
#15474=ORIENTED_EDGE ( 'NONE', *, *, #8485, .T. ) ;
#15475=ORIENTED_EDGE ( 'NONE', *, *, #15877, .T. ) ;
#15491=FACE_BOUND ( 'NONE', #22368, .T. ) ;
#15519=DIRECTION ( 'NONE',  ( 0.000000000000000000, 0.000000000000000000, 1.000000000000000000 ) ) ;
#15535=ORIENTED_EDGE ( 'NONE', *, *, #21970, .F. ) ;
#15536=DIRECTION ( 'NONE',  ( 0.000000000000000000, 0.000000000000000000, 1.000000000000000000 ) ) ;
#15549=ORIENTED_EDGE ( 'NONE', *, *, #22854, .T. ) ;
#15554=DIRECTION ( 'NONE',  ( 1.000000000000000000, 0.000000000000000000, 0.000000000000000000 ) ) ;
#15557=ADVANCED_FACE ( 'NONE', ( #10158, #9499 ), #22350, .F. ) ;
#15561=ORIENTED_EDGE ( 'NONE', *, *, #15885, .F. ) ;
#15580=DIRECTION ( 'NONE',  ( -1.000000000000000000, 0.000000000000000000, 0.000000000000000000 ) ) ;
#15590=VERTEX_POINT ( 'NONE', #3673 ) ;
#15592=DIRECTION ( 'NONE',  ( 0.9160001545545232160, -0.4011779117250717785, -0.000000000000000000 ) ) ;
#15596=CARTESIAN_POINT ( 'NONE',  ( 23.85000000000000497, 15.03999999999999915, -25.00000000000000000 ) ) ;
#15617=DIRECTION ( 'NONE',  ( 0.000000000000000000, 0.000000000000000000, 1.000000000000000000 ) ) ;
#15622=ORIENTED_EDGE ( 'NONE', *, *, #4652, .F. ) ;
#15625=ORIENTED_EDGE ( 'NONE', *, *, #7526, .F. ) ;
#15629=CARTESIAN_POINT ( 'NONE',  ( 29.00000000000000355, 29.50000000000000000, 27.00000000000000000 ) ) ;
#15634=VECTOR ( 'NONE', #4907, 1000.000000000000000 ) ;
#15644=CYLINDRICAL_SURFACE ( 'NONE', #10267, 5.100000000000000533 ) ;
#15647=EDGE_LOOP ( 'NONE', ( #9671, #13530, #4461 ) ) ;
#15661=AXIS2_PLACEMENT_3D ( 'NONE', #16365, #3207, #21874 ) ;
#15664=CARTESIAN_POINT ( 'NONE',  ( -16.99687406587155891, -7.923972684219721785, 5.245599057861376480 ) ) ;
#15665=DIRECTION ( 'NONE',  ( -0.000000000000000000, -0.000000000000000000, 1.000000000000000000 ) ) ;
#15669=CARTESIAN_POINT ( 'NONE',  ( 0.000000000000000000, 45.00000000000000000, 23.99999999999999645 ) ) ;
#15672=EDGE_LOOP ( 'NONE', ( #9419, #18881 ) ) ;
#15680=AXIS2_PLACEMENT_3D ( 'NONE', #14856, #11562, #11185 ) ;
#15692=ORIENTED_EDGE ( 'NONE', *, *, #9116, .F. ) ;
#15694=DIRECTION ( 'NONE',  ( -0.000000000000000000, -0.000000000000000000, -1.000000000000000000 ) ) ;
#15703=EDGE_CURVE ( 'NONE', #14530, #5080, #2321, .T. ) ;
#15731=CARTESIAN_POINT ( 'NONE',  ( 14.67173559926288462, -3.179195828807841018, -8.975010320294694921 ) ) ;
#15735=EDGE_CURVE ( 'NONE', #14640, #23460, #1300, .T. ) ;
#15743=FACE_OUTER_BOUND ( 'NONE', #14133, .T. ) ;
#15752=DIRECTION ( 'NONE',  ( -1.000000000000000000, 0.000000000000000000, 0.000000000000000000 ) ) ;
#15756=ORIENTED_EDGE ( 'NONE', *, *, #9611, .T. ) ;
#15757=DIRECTION ( 'NONE',  ( -0.000000000000000000, 0.000000000000000000, 1.000000000000000000 ) ) ;
#15772=AXIS2_PLACEMENT_3D ( 'NONE', #19392, #8754, #19762 ) ;
#15775=LINE ( 'NONE', #8453, #5134 ) ;
#15795=AXIS2_PLACEMENT_3D ( 'NONE', #8510, #4746, #15838 ) ;
#15796=EDGE_LOOP ( 'NONE', ( #18880, #19401 ) ) ;
#15802=DIRECTION ( 'NONE',  ( 0.000000000000000000, 0.000000000000000000, 1.000000000000000000 ) ) ;
#15805=CARTESIAN_POINT ( 'NONE',  ( 0.000000000000000000, 45.00000000000000000, 27.00000000000000000 ) ) ;
#15812=LINE ( 'NONE', #10173, #20636 ) ;
#15816=CARTESIAN_POINT ( 'NONE',  ( 17.59008829125738416, -9.499485695642603034, -0.4958780962348203203 ) ) ;
#15822=ORIENTED_EDGE ( 'NONE', *, *, #16647, .T. ) ;
#15833=CARTESIAN_POINT ( 'NONE',  ( 20.84999999999999432, -15.04000000000000448, 25.00000000000000000 ) ) ;
#15834=CARTESIAN_POINT ( 'NONE',  ( 20.85000000000000853, 15.03999999999999915, 27.00000000000000000 ) ) ;
#15837=CARTESIAN_POINT ( 'NONE',  ( 0.000000000000000000, 15.03999999999999915, 25.00000000000000000 ) ) ;
#15838=DIRECTION ( 'NONE',  ( -1.000000000000000000, 0.000000000000000000, 0.000000000000000000 ) ) ;
#15869=PLANE ( 'NONE',  #8638 ) ;
#15870=ORIENTED_EDGE ( 'NONE', *, *, #21191, .F. ) ;
#15877=EDGE_CURVE ( 'NONE', #6633, #15077, #5477, .T. ) ;
#15878=CARTESIAN_POINT ( 'NONE',  ( 31.10231664966676846, -45.36128193761570770, 27.00000000000000000 ) ) ;
#15885=EDGE_CURVE ( 'NONE', #18820, #704, #10829, .T. ) ;
#15895=CIRCLE ( 'NONE', #5381, 23.84999999999999432 ) ;
#15910=DIRECTION ( 'NONE',  ( -0.9160001545545232160, -0.4011779117250717785, 0.000000000000000000 ) ) ;
#15912=DIRECTION ( 'NONE',  ( 1.000000000000000000, 0.000000000000000000, 0.000000000000000000 ) ) ;
#15917=ORIENTED_EDGE ( 'NONE', *, *, #1411, .F. ) ;
#15918=ORIENTED_EDGE ( 'NONE', *, *, #10682, .F. ) ;
#15919=DIRECTION ( 'NONE',  ( -1.000000000000000000, 0.000000000000000000, 0.000000000000000000 ) ) ;
#15923=ORIENTED_EDGE ( 'NONE', *, *, #7420, .T. ) ;
#15934=CARTESIAN_POINT ( 'NONE',  ( 15.00000000000000000, 6.781880092842756171E-15, 9.499999999999987566 ) ) ;
#15946=DIRECTION ( 'NONE',  ( -0.000000000000000000, 0.000000000000000000, -1.000000000000000000 ) ) ;
#15950=FACE_OUTER_BOUND ( 'NONE', #11910, .T. ) ;
#15953=AXIS2_PLACEMENT_3D ( 'NONE', #12126, #21058, #19369 ) ;
#15957=VERTEX_POINT ( 'NONE', #113 ) ;
#15973=CARTESIAN_POINT ( 'NONE',  ( 18.49999999999999645, -15.23000000000000043, -27.00000000000000000 ) ) ;
#15990=VERTEX_POINT ( 'NONE', #22664 ) ;
#15992=ORIENTED_EDGE ( 'NONE', *, *, #8485, .F. ) ;
#15998=CARTESIAN_POINT ( 'NONE',  ( 39.99999999999999289, 29.50000000000000000, -27.00000000000000000 ) ) ;
#16005=CARTESIAN_POINT ( 'NONE',  ( -40.89823313241237912, 26.41789760203348081, -27.00000000000000000 ) ) ;
#16007=ADVANCED_FACE ( 'NONE', ( #2406 ), #11915, .F. ) ;
#16019=CARTESIAN_POINT ( 'NONE',  ( -39.99999999999999289, 29.50000000000000000, -27.00000000000000000 ) ) ;
#16028=CIRCLE ( 'NONE', #8210, 11.00000000000000355 ) ;
#16030=CARTESIAN_POINT ( 'NONE',  ( -17.57797814737053699, -9.461914562436920306, 0.9781177603712988278 ) ) ;
#16034=ADVANCED_FACE ( 'NONE', ( #20966 ), #19019, .F. ) ;
#16035=PLANE ( 'NONE',  #12040 ) ;
#16038=CARTESIAN_POINT ( 'NONE',  ( 15.00000000000000000, 5.618453542512190434E-15, -9.499999999999987566 ) ) ;
#16043=CARTESIAN_POINT ( 'NONE',  ( 17.38700629636781869, -8.908123924593978060, -3.336041480784311286 ) ) ;
#16044=CARTESIAN_POINT ( 'NONE',  ( 14.79227890392045097, 2.568991289487080110, 9.169086800441901275 ) ) ;
#16059=PLANE ( 'NONE',  #17732 ) ;
#16082=ORIENTED_EDGE ( 'NONE', *, *, #2239, .T. ) ;
#16090=CONICAL_SURFACE ( 'NONE', #11785, 2.024999999999999911, 0.7853981633974743692 ) ;
#16099=EDGE_CURVE ( 'NONE', #20120, #13548, #2891, .T. ) ;
#16106=DIRECTION ( 'NONE',  ( -0.000000000000000000, -0.000000000000000000, -1.000000000000000000 ) ) ;
#16108=CARTESIAN_POINT ( 'NONE',  ( 23.85000000000000497, 15.03999999999999915, 25.00000000000000000 ) ) ;
#16124=DIRECTION ( 'NONE',  ( -0.000000000000000000, 0.000000000000000000, -1.000000000000000000 ) ) ;
#16140=ORIENTED_EDGE ( 'NONE', *, *, #18777, .F. ) ;
#16142=CARTESIAN_POINT ( 'NONE',  ( 18.49999999999999645, -15.23000000000000043, 27.00000000000000000 ) ) ;
#16145=DIRECTION ( 'NONE',  ( 0.000000000000000000, -1.000000000000000000, 0.000000000000000000 ) ) ;
#16148=LINE ( 'NONE', #8695, #2788 ) ;
#16151=EDGE_CURVE ( 'NONE', #8356, #21663, #18022, .T. ) ;
#16154=ORIENTED_EDGE ( 'NONE', *, *, #14548, .T. ) ;
#16163=CARTESIAN_POINT ( 'NONE',  ( -16.19099482616364583, -6.271157271432198144, -7.149633965064782437 ) ) ;
#16171=CARTESIAN_POINT ( 'NONE',  ( -23.89999999999999858, -29.50000000000001066, 27.00000000000000000 ) ) ;
#16175=CARTESIAN_POINT ( 'NONE',  ( 17.38971744193258573, -8.915620082851736683, 3.315798060087240096 ) ) ;
#16177=VECTOR ( 'NONE', #20253, 1000.000000000000000 ) ;
#16194=CIRCLE ( 'NONE', #22441, 23.85000000000000497 ) ;
#16198=VECTOR ( 'NONE', #17626, 1000.000000000000000 ) ;
#16200=VECTOR ( 'NONE', #6400, 1000.000000000000000 ) ;
#16201=CYLINDRICAL_SURFACE ( 'NONE', #2836, 1.999999999999994449 ) ;
#16203=DIRECTION ( 'NONE',  ( 4.613626265895763066E-16, 1.000000000000000000, -0.000000000000000000 ) ) ;
#16206=CARTESIAN_POINT ( 'NONE',  ( 16.68233279685676251, 7.225448002938849257, 6.184784653374919117 ) ) ;
#16212=DIRECTION ( 'NONE',  ( 1.000000000000000000, 0.000000000000000000, 0.000000000000000000 ) ) ;
#16225=DIRECTION ( 'NONE',  ( 0.7071067811865500152, 8.659560562354902043E-17, 0.7071067811865450192 ) ) ;
#16240=VERTEX_POINT ( 'NONE', #5700 ) ;
#16241=CARTESIAN_POINT ( 'NONE',  ( -40.89823313241237912, -26.41789760203349502, -27.00000000000000000 ) ) ;
#16245=FACE_OUTER_BOUND ( 'NONE', #21043, .T. ) ;
#16250=B_SPLINE_CURVE_WITH_KNOTS ( 'NONE', 3,
 ( #16654, #21905, #9206, #5544, #9078, #23851, #11137, #20089 ),
 .UNSPECIFIED., .F., .F.,
 ( 4, 2, 2, 4 ),
 ( 0.003892319173193285655, 0.004864202078960310274, 0.005836084984727334460, 0.007779850796261383698 ),
 .UNSPECIFIED. ) ;
#16251=DIRECTION ( 'NONE',  ( -1.000000000000000000, 0.000000000000000000, 0.000000000000000000 ) ) ;
#16258=EDGE_CURVE ( 'NONE', #22631, #721, #9437, .T. ) ;
#16265=DIRECTION ( 'NONE',  ( -0.000000000000000000, -0.000000000000000000, -1.000000000000000000 ) ) ;
#16277=ORIENTED_EDGE ( 'NONE', *, *, #16470, .F. ) ;
#16278=DIRECTION ( 'NONE',  ( 1.000000000000000000, 0.000000000000000000, 0.000000000000000000 ) ) ;
#16283=CARTESIAN_POINT ( 'NONE',  ( 0.000000000000000000, 45.00000000000000000, 23.99999999999999645 ) ) ;
#16297=ORIENTED_EDGE ( 'NONE', *, *, #12223, .T. ) ;
#16310=ORIENTED_EDGE ( 'NONE', *, *, #8076, .F. ) ;
#16313=CARTESIAN_POINT ( 'NONE',  ( 17.38971744193259994, 8.915620082851745565, -3.315798060087243648 ) ) ;
#16320=ORIENTED_EDGE ( 'NONE', *, *, #6502, .F. ) ;
#16323=LINE ( 'NONE', #12529, #20907 ) ;
#16338=CARTESIAN_POINT ( 'NONE',  ( -40.89823313241237912, 26.41789760203348081, -27.00000000000000000 ) ) ;
#16346=CARTESIAN_POINT ( 'NONE',  ( 1.999999999999994449, -45.00000000000000000, 23.99999999999999645 ) ) ;
#16347=VERTEX_POINT ( 'NONE', #691 ) ;
#16349=CARTESIAN_POINT ( 'NONE',  ( 14.51962751333974389, -3.765689428759035895, 27.00000000000000000 ) ) ;
#16351=DIRECTION ( 'NONE',  ( 1.000000000000000000, 0.000000000000000000, 0.000000000000000000 ) ) ;
#16359=CARTESIAN_POINT ( 'NONE',  ( -39.99999999999999289, 29.50000000000000000, 27.00000000000000000 ) ) ;
#16363=EDGE_CURVE ( 'NONE', #19575, #19379, #20034, .T. ) ;
#16365=CARTESIAN_POINT ( 'NONE',  ( 0.000000000000000000, -45.00000000000000000, 26.97499999999999432 ) ) ;
#16371=EDGE_LOOP ( 'NONE', ( #22132, #13536, #20643, #6649 ) ) ;
#16381=DIRECTION ( 'NONE',  ( -0.000000000000000000, -0.000000000000000000, 1.000000000000000000 ) ) ;
#16398=CARTESIAN_POINT ( 'NONE',  ( 0.000000000000000000, 15.03999999999999915, -25.00000000000000000 ) ) ;
#16405=VECTOR ( 'NONE', #8537, 1000.000000000000000 ) ;
#16422=CARTESIAN_POINT ( 'NONE',  ( 17.57797814737054409, 9.461914562436920306, 0.9781177603712970514 ) ) ;
#16428=CARTESIAN_POINT ( 'NONE',  ( -39.99999999999999289, -29.50000000000001066, -27.00000000000000000 ) ) ;
#16442=AXIS2_PLACEMENT_3D ( 'NONE', #11292, #2, #22098 ) ;
#16443=LINE ( 'NONE', #1227, #1434 ) ;
#16452=PLANE ( 'NONE',  #11411 ) ;
#16461=CIRCLE ( 'NONE', #7113, 2.024999999999999911 ) ;
#16470=EDGE_CURVE ( 'NONE', #10631, #14244, #178, .T. ) ;
#16473=AXIS2_PLACEMENT_3D ( 'NONE', #4971, #19845, #4720 ) ;
#16478=AXIS2_PLACEMENT_3D ( 'NONE', #7549, #13054, #7325 ) ;
#16495=DIRECTION ( 'NONE',  ( 1.000000000000000000, 0.000000000000000000, 0.000000000000000000 ) ) ;
#16496=ADVANCED_FACE ( 'NONE', ( #17502 ), #23270, .F. ) ;
#16502=CARTESIAN_POINT ( 'NONE',  ( -41.99999999999999289, -25.93535998569255341, -27.00000000000000000 ) ) ;
#16505=VERTEX_POINT ( 'NONE', #14088 ) ;
#16514=AXIS2_PLACEMENT_3D ( 'NONE', #13893, #23654, #10194 ) ;
#16515=CARTESIAN_POINT ( 'NONE',  ( 0.000000000000000000, -15.03999999999999915, -27.00000000000000000 ) ) ;
#16529=ORIENTED_EDGE ( 'NONE', *, *, #8354, .F. ) ;
#16530=VECTOR ( 'NONE', #18219, 1000.000000000000000 ) ;
#16534=AXIS2_PLACEMENT_3D ( 'NONE', #2146, #18994, #14717 ) ;
#16535=EDGE_CURVE ( 'NONE', #9670, #5201, #11441, .T. ) ;
#16538=VERTEX_POINT ( 'NONE', #10047 ) ;
#16548=ORIENTED_EDGE ( 'NONE', *, *, #3888, .F. ) ;
#16552=CARTESIAN_POINT ( 'NONE',  ( 0.000000000000000000, 45.00000000000000000, -26.97499999999999432 ) ) ;
#16561=EDGE_CURVE ( 'NONE', #21442, #13963, #14821, .T. ) ;
#16576=DIRECTION ( 'NONE',  ( -0.000000000000000000, -0.000000000000000000, -1.000000000000000000 ) ) ;
#16590=CARTESIAN_POINT ( 'NONE',  ( -14.79187224938325507, 2.570168443617186771, 9.168425918763430715 ) ) ;
#16597=FACE_BOUND ( 'NONE', #2410, .T. ) ;
#16598=DIRECTION ( 'NONE',  ( 0.000000000000000000, 0.000000000000000000, 1.000000000000000000 ) ) ;
#16612=DIRECTION ( 'NONE',  ( -1.000000000000000000, 0.000000000000000000, 0.000000000000000000 ) ) ;
#16623=ORIENTED_EDGE ( 'NONE', *, *, #19855, .F. ) ;
#16629=VERTEX_POINT ( 'NONE', #4443 ) ;
#16647=EDGE_CURVE ( 'NONE', #18868, #23464, #10271, .T. ) ;
#16654=CARTESIAN_POINT ( 'NONE',  ( -14.99999999999999822, 6.045577542124163753E-21, -9.499999999999994671 ) ) ;
#16658=ORIENTED_EDGE ( 'NONE', *, *, #7102, .T. ) ;
#16672=CARTESIAN_POINT ( 'NONE',  ( 0.000000000000000000, 45.00000000000000000, 26.97499999999999432 ) ) ;
#16674=EDGE_LOOP ( 'NONE', ( #22880, #22396, #23129, #12530 ) ) ;
#16679=EDGE_CURVE ( 'NONE', #4095, #22047, #20048, .T. ) ;
#16688=AXIS2_PLACEMENT_3D ( 'NONE', #3745, #13496, #87 ) ;
#16691=AXIS2_PLACEMENT_3D ( 'NONE', #7222, #18221, #16612 ) ;
#16692=ORIENTED_EDGE ( 'NONE', *, *, #12702, .T. ) ;
#16716=DIRECTION ( 'NONE',  ( 1.000000000000000000, 0.000000000000000000, 0.000000000000000000 ) ) ;
#16723=AXIS2_PLACEMENT_3D ( 'NONE', #8593, #14328, #12617 ) ;
#16734=ORIENTED_EDGE ( 'NONE', *, *, #7702, .T. ) ;
#16735=ORIENTED_EDGE ( 'NONE', *, *, #21250, .T. ) ;
#16741=EDGE_CURVE ( 'NONE', #4173, #20705, #1737, .T. ) ;
#16743=VERTEX_POINT ( 'NONE', #16359 ) ;
#16758=ADVANCED_FACE ( 'NONE', ( #18577 ), #23944, .F. ) ;
#16762=CYLINDRICAL_SURFACE ( 'NONE', #10319, 4.999999999999997335 ) ;
#16765=AXIS2_PLACEMENT_3D ( 'NONE', #19487, #8600, #21684 ) ;
#16772=DIRECTION ( 'NONE',  ( -1.000000000000000000, 0.000000000000000000, 0.000000000000000000 ) ) ;
#16801=CARTESIAN_POINT ( 'NONE',  ( -23.84999999999999432, -15.03999999999999915, -25.00000000000000000 ) ) ;
#16831=DIRECTION ( 'NONE',  ( 0.000000000000000000, 0.000000000000000000, -1.000000000000000000 ) ) ;
#16845=EDGE_CURVE ( 'NONE', #10814, #14, #10687, .T. ) ;
#16846=CARTESIAN_POINT ( 'NONE',  ( -28.99999999999999645, 29.50000000000000000, 27.00000000000000000 ) ) ;
#16853=EDGE_LOOP ( 'NONE', ( #17641, #529, #13760, #16154 ) ) ;
#16857=VECTOR ( 'NONE', #4267, 1000.000000000000000 ) ;
#16864=DIRECTION ( 'NONE',  ( -1.000000000000000000, 0.000000000000000000, 0.000000000000000000 ) ) ;
#16874=CARTESIAN_POINT ( 'NONE',  ( -23.85000000000000497, 15.03999999999999915, -25.00000000000000000 ) ) ;
#16879=VECTOR ( 'NONE', #21648, 1000.000000000000000 ) ;
#16880=AXIS2_PLACEMENT_3D ( 'NONE', #11984, #544, #19207 ) ;
#16883=ORIENTED_EDGE ( 'NONE', *, *, #19440, .F. ) ;
#16911=CARTESIAN_POINT ( 'NONE',  ( 17.06033556854819011, 8.068938288216807919, -5.036196554528634017 ) ) ;
#16918=ORIENTED_EDGE ( 'NONE', *, *, #19336, .F. ) ;
#16933=EDGE_CURVE ( 'NONE', #6874, #7931, #13062, .T. ) ;
#16938=CARTESIAN_POINT ( 'NONE',  ( -17.38971744193260349, 8.915620082851750894, 3.315798060087249421 ) ) ;
#16951=CONICAL_SURFACE ( 'NONE', #617, 10.50249999999999950, 0.7853981633974447263 ) ;
#16954=DIRECTION ( 'NONE',  ( 0.000000000000000000, 0.000000000000000000, -1.000000000000000000 ) ) ;
#16965=FACE_BOUND ( 'NONE', #23330, .T. ) ;
#16969=ADVANCED_FACE ( 'NONE', ( #6453 ), #23963, .F. ) ;
#16996=EDGE_CURVE ( 'NONE', #3894, #5827, #4121, .T. ) ;
#17013=CYLINDRICAL_SURFACE ( 'NONE', #3758, 18.50000000000000000 ) ;
#17014=ORIENTED_EDGE ( 'NONE', *, *, #186, .F. ) ;
#17027=ORIENTED_EDGE ( 'NONE', *, *, #3412, .T. ) ;
#17028=FACE_OUTER_BOUND ( 'NONE', #11514, .T. ) ;
#17041=LINE ( 'NONE', #15082, #19072 ) ;
#17048=CARTESIAN_POINT ( 'NONE',  ( 0.000000000000000000, -45.00000000000000000, 27.00000000000000000 ) ) ;
#17054=LINE ( 'NONE', #7765, #5935 ) ;
#17055=CARTESIAN_POINT ( 'NONE',  ( 0.000000000000000000, 0.000000000000000000, -27.00000000000000000 ) ) ;
#17057=CARTESIAN_POINT ( 'NONE',  ( -15.57833309066360705, 5.219313726039665369, -7.987432870209370428 ) ) ;
#17079=ORIENTED_EDGE ( 'NONE', *, *, #14215, .F. ) ;
#17089=ORIENTED_EDGE ( 'NONE', *, *, #9581, .F. ) ;
#17092=CARTESIAN_POINT ( 'NONE',  ( -23.85000000000000497, 15.03999999999999915, -25.00000000000000000 ) ) ;
#17101=FACE_OUTER_BOUND ( 'NONE', #12097, .T. ) ;
#17111=CYLINDRICAL_SURFACE ( 'NONE', #7086, 9.499999999999994671 ) ;
#17115=ORIENTED_EDGE ( 'NONE', *, *, #18777, .T. ) ;
#17116=DIRECTION ( 'NONE',  ( 4.613626265895764052E-16, -1.000000000000000000, 0.000000000000000000 ) ) ;
#17124=AXIS2_PLACEMENT_3D ( 'NONE', #23017, #23278, #6551 ) ;
#17128=ORIENTED_EDGE ( 'NONE', *, *, #6127, .T. ) ;
#17141=DIRECTION ( 'NONE',  ( -1.000000000000000000, -0.000000000000000000, -0.000000000000000000 ) ) ;
#17166=ORIENTED_EDGE ( 'NONE', *, *, #6502, .T. ) ;
#17167=ADVANCED_BREP_SHAPE_REPRESENTATION ( '', ( #10155, #8005 ), #20496 ) ;
#17200=DIRECTION ( 'NONE',  ( -1.000000000000000000, 0.000000000000000000, 0.000000000000000000 ) ) ;
#17204=ADVANCED_FACE ( 'NONE', ( #2758 ), #8491, .F. ) ;
#17208=VECTOR ( 'NONE', #4541, 1000.000000000000000 ) ;
#17211=EDGE_CURVE ( 'NONE', #11604, #23403, #10425, .T. ) ;
#17212=VECTOR ( 'NONE', #19052, 1000.000000000000000 ) ;
#17217=CARTESIAN_POINT ( 'NONE',  ( -41.99999999999999289, 0.000000000000000000, 0.000000000000000000 ) ) ;
#17219=ORIENTED_EDGE ( 'NONE', *, *, #21052, .T. ) ;
#17221=CARTESIAN_POINT ( 'NONE',  ( 41.99999999999999289, 5.618459588085056979E-15, 0.000000000000000000 ) ) ;
#17226=CIRCLE ( 'NONE', #20359, 14.99999999999999822 ) ;
#17234=DIRECTION ( 'NONE',  ( -0.000000000000000000, -0.000000000000000000, -1.000000000000000000 ) ) ;
#17242=ADVANCED_FACE ( 'NONE', ( #21060, #8109 ), #11763, .T. ) ;
#17243=ORIENTED_EDGE ( 'NONE', *, *, #16647, .F. ) ;
#17244=EDGE_CURVE ( 'NONE', #14989, #16538, #4048, .T. ) ;
#17247=ORIENTED_EDGE ( 'NONE', *, *, #3669, .T. ) ;
#17250=ORIENTED_EDGE ( 'NONE', *, *, #16741, .T. ) ;
#17259=ORIENTED_EDGE ( 'NONE', *, *, #992, .F. ) ;
#17260=DIRECTION ( 'NONE',  ( -1.000000000000000000, 0.000000000000000000, 0.000000000000000000 ) ) ;
#17271=DIRECTION ( 'NONE',  ( 4.613626265895764052E-16, 1.000000000000000000, 0.000000000000000000 ) ) ;
#17273=LINE ( 'NONE', #18874, #9121 ) ;
#17283=VERTEX_POINT ( 'NONE', #8846 ) ;
#17293=ORIENTED_EDGE ( 'NONE', *, *, #24009, .F. ) ;
#17296=VECTOR ( 'NONE', #20578, 1000.000000000000000 ) ;
#17307=B_SPLINE_CURVE_WITH_KNOTS ( 'NONE', 3,
 ( #4415, #11827, #2083, #22486, #5762, #9637, #13177, #20635 ),
 .UNSPECIFIED., .F., .F.,
 ( 4, 2, 2, 4 ),
 ( 4.336808689942017736E-19, 0.001946159586596638924, 0.002919239379894958061, 0.003892319173193277415 ),
 .UNSPECIFIED. ) ;
#17309=ORIENTED_EDGE ( 'NONE', *, *, #13419, .F. ) ;
#17330=ORIENTED_EDGE ( 'NONE', *, *, #4003, .T. ) ;
#17332=DIRECTION ( 'NONE',  ( -0.000000000000000000, -0.000000000000000000, -1.000000000000000000 ) ) ;
#17339=CONICAL_SURFACE ( 'NONE', #18898, 2.024999999999999911, 0.7853981633974743692 ) ;
#17343=ORIENTED_EDGE ( 'NONE', *, *, #23666, .T. ) ;
#17344=PLANE ( 'NONE',  #17949 ) ;
#17363=ORIENTED_EDGE ( 'NONE', *, *, #20845, .F. ) ;
#17377=B_SPLINE_CURVE_WITH_KNOTS ( 'NONE', 3,
 ( #7891, #2184, #17057, #15341, #20613, #22812, #357, #2056, #6091, #18663, #7769, #252, #20370, #1833, #9480, #7411, #22329, #22455, #5611, #13033, #20494, #1937, #9352, #16938, #124, #5735, #3891, #18769, #7658, #23046, #22933, #6208, #21218, #4523, #20976, #10344 ),
 .UNSPECIFIED., .F., .F.,
 ( 4, 2, 2, 2, 2, 2, 2, 2, 2, 2, 2, 2, 2, 2, 2, 2, 2, 4 ),
 ( 4.249187360970369464E-18, 0.002901772246161924990, 0.003627215307702405262, 0.004352658369242885100, 0.005803544492323838705, 0.006528987553864317242, 0.007254430615404792310, 0.008705316738485749384, 0.01015620286156670646, 0.01160708898464766527, 0.01305797510772862408, 0.01450886123080957942, 0.01595974735389053822, 0.01741063347697149530, 0.01886151960005245584, 0.02031240572313341639, 0.02176329184621437693, 0.02321417796929533747 ),
 .UNSPECIFIED. ) ;
#17390=CARTESIAN_POINT ( 'NONE',  ( -14.91530227160598621, -1.623290104782665999, -9.365835742197237579 ) ) ;
#17392=ORIENTED_EDGE ( 'NONE', *, *, #21970, .T. ) ;
#17393=CARTESIAN_POINT ( 'NONE',  ( -31.10231664966676135, 45.36128193761570770, 27.00000000000000000 ) ) ;
#17408=ORIENTED_EDGE ( 'NONE', *, *, #21007, .F. ) ;
#17409=DIRECTION ( 'NONE',  ( -1.000000000000000000, 0.000000000000000000, 0.000000000000000000 ) ) ;
#17410=ORIENTED_EDGE ( 'NONE', *, *, #16363, .T. ) ;
#17426=DIRECTION ( 'NONE',  ( -1.000000000000000000, 0.000000000000000000, 0.000000000000000000 ) ) ;
#17444=DIRECTION ( 'NONE',  ( 1.000000000000000000, 0.000000000000000000, 0.000000000000000000 ) ) ;
#17446=LINE ( 'NONE', #20745, #3580 ) ;
#17448=ORIENTED_EDGE ( 'NONE', *, *, #14379, .T. ) ;
#17457=CARTESIAN_POINT ( 'NONE',  ( 29.00000000000000355, 29.50000000000000000, -27.00000000000000000 ) ) ;
#17458=FACE_OUTER_BOUND ( 'NONE', #4658, .T. ) ;
#17466=FACE_OUTER_BOUND ( 'NONE', #16853, .T. ) ;
#17473=CARTESIAN_POINT ( 'NONE',  ( 23.90000000000000568, 29.50000000000000000, -27.00000000000000000 ) ) ;
#17495=EDGE_CURVE ( 'NONE', #23345, #7541, #22749, .T. ) ;
#17502=FACE_OUTER_BOUND ( 'NONE', #947, .T. ) ;
#17509=EDGE_LOOP ( 'NONE', ( #13794, #1643, #6446, #1570, #9693, #303 ) ) ;
#17527=VERTEX_POINT ( 'NONE', #19086 ) ;
#17535=DIRECTION ( 'NONE',  ( 0.000000000000000000, 0.000000000000000000, 1.000000000000000000 ) ) ;
#17537=DIRECTION ( 'NONE',  ( 1.000000000000000000, 0.000000000000000000, 0.000000000000000000 ) ) ;
#17543=ORIENTED_EDGE ( 'NONE', *, *, #6657, .T. ) ;
#17554=CARTESIAN_POINT ( 'NONE',  ( 0.000000000000000000, -15.03999999999999915, -25.00000000000000000 ) ) ;
#17563=LINE ( 'NONE', #12063, #12179 ) ;
#17565=FACE_OUTER_BOUND ( 'NONE', #5448, .T. ) ;
#17578=AXIS2_PLACEMENT_3D ( 'NONE', #11821, #2583, #9994 ) ;
#17607=VERTEX_POINT ( 'NONE', #2620 ) ;
#17617=CIRCLE ( 'NONE', #20743, 5.100000000000000533 ) ;
#17621=CARTESIAN_POINT ( 'NONE',  ( -16.08510323282434129, -6.088885580147182175, 7.295537496892092300 ) ) ;
#17624=DIRECTION ( 'NONE',  ( 1.000000000000000000, 0.000000000000000000, 0.000000000000000000 ) ) ;
#17626=DIRECTION ( 'NONE',  ( -1.000000000000000000, -0.000000000000000000, -0.000000000000000000 ) ) ;
#17632=CARTESIAN_POINT ( 'NONE',  ( 17.15849686392982676, -8.309918483244977949, 4.628645577532783051 ) ) ;
#17634=CARTESIAN_POINT ( 'NONE',  ( 14.51962751333974389, 3.765689428759029234, 8.721787840009197268 ) ) ;
#17641=ORIENTED_EDGE ( 'NONE', *, *, #12223, .F. ) ;
#17654=CARTESIAN_POINT ( 'NONE',  ( 14.51962751333974389, 3.765689428759029234, -27.00000000000000000 ) ) ;
#17657=CIRCLE ( 'NONE', #23907, 2.024999999999999911 ) ;
#17669=DIRECTION ( 'NONE',  ( -0.000000000000000000, -0.000000000000000000, -1.000000000000000000 ) ) ;
#17672=LINE ( 'NONE', #973, #18855 ) ;
#17681=ORIENTED_EDGE ( 'NONE', *, *, #2798, .T. ) ;
#17699=DIRECTION ( 'NONE',  ( -1.000000000000000000, 0.000000000000000000, 0.000000000000000000 ) ) ;
#17702=VECTOR ( 'NONE', #11809, 1000.000000000000114 ) ;
#17721=ORIENTED_EDGE ( 'NONE', *, *, #4061, .T. ) ;
#17722=DIRECTION ( 'NONE',  ( -1.000000000000000000, 0.000000000000000000, 0.000000000000000000 ) ) ;
#17732=AXIS2_PLACEMENT_3D ( 'NONE', #23523, #15946, #6805 ) ;
#17736=DIRECTION ( 'NONE',  ( 0.9160001545545232160, -0.4011779117250717785, 0.000000000000000000 ) ) ;
#17751=VECTOR ( 'NONE', #3539, 1000.000000000000000 ) ;
#17762=CARTESIAN_POINT ( 'NONE',  ( -16.81886298599061647, -7.518780870797758809, 5.825851398835388828 ) ) ;
#17767=DIRECTION ( 'NONE',  ( -0.000000000000000000, -0.000000000000000000, 1.000000000000000000 ) ) ;
#17791=EDGE_CURVE ( 'NONE', #11663, #22613, #10869, .T. ) ;
#17797=FACE_OUTER_BOUND ( 'NONE', #18752, .T. ) ;
#17801=CARTESIAN_POINT ( 'NONE',  ( -1.999999999999994449, 45.00000000000000000, -26.97499999999999432 ) ) ;
#17814=ORIENTED_EDGE ( 'NONE', *, *, #4500, .T. ) ;
#17817=ORIENTED_EDGE ( 'NONE', *, *, #6603, .T. ) ;
#17820=CARTESIAN_POINT ( 'NONE',  ( 0.000000000000000000, -45.00000000000000000, -27.00000000000000000 ) ) ;
#17844=LINE ( 'NONE', #16349, #11353 ) ;
#17851=EDGE_LOOP ( 'NONE', ( #15116, #12707, #13706, #15625 ) ) ;
#17857=ORIENTED_EDGE ( 'NONE', *, *, #11836, .T. ) ;
#17859=EDGE_LOOP ( 'NONE', ( #12589, #21181, #19624, #23602 ) ) ;
#17864=CARTESIAN_POINT ( 'NONE',  ( 40.89823313241237912, 26.41789760203348081, 27.00000000000000000 ) ) ;
#17869=CARTESIAN_POINT ( 'NONE',  ( 23.90000000000000568, 29.50000000000000000, 27.00000000000000000 ) ) ;
#17881=DIRECTION ( 'NONE',  ( -0.000000000000000000, -0.000000000000000000, 1.000000000000000000 ) ) ;
#17882=CARTESIAN_POINT ( 'NONE',  ( -14.98950073861089294, -0.6491375924673344899, -9.483449329262338523 ) ) ;
#17886=VERTEX_POINT ( 'NONE', #1515 ) ;
#17893=FACE_OUTER_BOUND ( 'NONE', #12397, .T. ) ;
#17895=CARTESIAN_POINT ( 'NONE',  ( 16.18147534945000032, -6.260849737139246862, -7.148624562014513906 ) ) ;
#17923=DIRECTION ( 'NONE',  ( -0.8571673007021116675, 0.000000000000000000, -0.5150380749100552658 ) ) ;
#17927=ORIENTED_EDGE ( 'NONE', *, *, #10940, .T. ) ;
#17934=ORIENTED_EDGE ( 'NONE', *, *, #20066, .F. ) ;
#17943=LINE ( 'NONE', #6718, #15634 ) ;
#17945=DIRECTION ( 'NONE',  ( -1.000000000000000000, 0.000000000000000000, 0.000000000000000000 ) ) ;
#17946=CARTESIAN_POINT ( 'NONE',  ( -41.49999999999999289, 27.79189783386526358, -27.00000000000000000 ) ) ;
#17949=AXIS2_PLACEMENT_3D ( 'NONE', #13939, #646, #15757 ) ;
#17972=CARTESIAN_POINT ( 'NONE',  ( -20.85000000000000142, -15.03999999999999915, -25.00000000000000000 ) ) ;
#17975=EDGE_LOOP ( 'NONE', ( #16320, #16297, #1723, #21983 ) ) ;
#17978=DIRECTION ( 'NONE',  ( -0.4011779117250717785, -0.9160001545545232160, 0.000000000000000000 ) ) ;
#17985=DIRECTION ( 'NONE',  ( 0.8571673007021116675, 1.049727191138617833E-16, -0.5150380749100552658 ) ) ;
#17991=ADVANCED_FACE ( 'NONE', ( #15243 ), #5861, .F. ) ;
#17993=ORIENTED_EDGE ( 'NONE', *, *, #9451, .T. ) ;
#17994=CARTESIAN_POINT ( 'NONE',  ( -17.38971744193259994, -8.915620082851749117, -3.315798060087244981 ) ) ;
#18004=CARTESIAN_POINT ( 'NONE',  ( 30.44534269664590909, -40.40463133211080304, -27.00000000000000000 ) ) ;
#18005=CARTESIAN_POINT ( 'NONE',  ( 15.57833309066359817, -5.219313726039669810, -7.987432870209351776 ) ) ;
#18010=ORIENTED_EDGE ( 'NONE', *, *, #3499, .F. ) ;
#18011=AXIS2_PLACEMENT_3D ( 'NONE', #22069, #12769, #10568 ) ;
#18022=LINE ( 'NONE', #1318, #9880 ) ;
#18037=DIRECTION ( 'NONE',  ( 0.000000000000000000, 0.000000000000000000, 1.000000000000000000 ) ) ;
#18040=DIRECTION ( 'NONE',  ( 0.8571673007021116675, 1.049727191138617833E-16, -0.5150380749100552658 ) ) ;
#18048=EDGE_LOOP ( 'NONE', ( #20963, #6405, #3846, #634 ) ) ;
#18049=DIRECTION ( 'NONE',  ( -0.9160001545545232160, -0.4011779117250717785, 0.000000000000000000 ) ) ;
#18051=AXIS2_PLACEMENT_3D ( 'NONE', #5761, #13176, #4547 ) ;
#18093=CARTESIAN_POINT ( 'NONE',  ( -41.49999999999999289, -27.79189783386527779, 27.00000000000000000 ) ) ;
#18100=DIRECTION ( 'NONE',  ( -0.000000000000000000, -0.000000000000000000, -1.000000000000000000 ) ) ;
#18110=CYLINDRICAL_SURFACE ( 'NONE', #18416, 18.49999999999999645 ) ;
#18120=AXIS2_PLACEMENT_3D ( 'NONE', #6579, #19868, #17537 ) ;
#18122=EDGE_CURVE ( 'NONE', #5301, #7700, #19176, .T. ) ;
#18128=CARTESIAN_POINT ( 'NONE',  ( -31.10231664966676135, 45.36128193761570770, 27.00000000000000000 ) ) ;
#18150=EDGE_CURVE ( 'NONE', #19513, #11923, #14421, .T. ) ;
#18157=CARTESIAN_POINT ( 'NONE',  ( 40.00000000000000000, -29.50000000000000000, -27.00000000000000000 ) ) ;
#18166=CARTESIAN_POINT ( 'NONE',  ( 17.57831567727901145, 9.462949834988604536, -0.9681625741885153680 ) ) ;
#18168=ORIENTED_EDGE ( 'NONE', *, *, #22771, .F. ) ;
#18188=ADVANCED_FACE ( 'NONE', ( #11962 ), #17344, .T. ) ;
#18192=AXIS2_PLACEMENT_3D ( 'NONE', #13725, #15665, #6420 ) ;
#18196=FACE_BOUND ( 'NONE', #2394, .T. ) ;
#18200=DIRECTION ( 'NONE',  ( -0.000000000000000000, -0.000000000000000000, 1.000000000000000000 ) ) ;
#18207=ORIENTED_EDGE ( 'NONE', *, *, #12702, .F. ) ;
#18219=DIRECTION ( 'NONE',  ( -0.000000000000000000, -0.000000000000000000, -1.000000000000000000 ) ) ;
#18221=DIRECTION ( 'NONE',  ( -0.000000000000000000, -0.000000000000000000, -1.000000000000000000 ) ) ;
#18226=VERTEX_POINT ( 'NONE', #8304 ) ;
#18228=EDGE_CURVE ( 'NONE', #18226, #10247, #1198, .T. ) ;
#18241=VERTEX_POINT ( 'NONE', #16428 ) ;
#18249=AXIS2_PLACEMENT_3D ( 'NONE', #5672, #3830, #1987 ) ;
#18252=CYLINDRICAL_SURFACE ( 'NONE', #1702, 20.85000000000000853 ) ;
#18259=CARTESIAN_POINT ( 'NONE',  ( -28.99999999999999645, -29.50000000000001066, -27.00000000000000000 ) ) ;
#18268=DIRECTION ( 'NONE',  ( 0.000000000000000000, 0.000000000000000000, -1.000000000000000000 ) ) ;
#18269=EDGE_LOOP ( 'NONE', ( #13102, #13635, #12071 ) ) ;
#18279=DIRECTION ( 'NONE',  ( -1.000000000000000000, 0.000000000000000000, 0.000000000000000000 ) ) ;
#18290=ORIENTED_EDGE ( 'NONE', *, *, #2608, .F. ) ;
#18291=ORIENTED_EDGE ( 'NONE', *, *, #12676, .T. ) ;
#18297=DIRECTION ( 'NONE',  ( -0.000000000000000000, -0.000000000000000000, 1.000000000000000000 ) ) ;
#18317=EDGE_LOOP ( 'NONE', ( #16883, #20887, #9159, #5326 ) ) ;
#18319=CARTESIAN_POINT ( 'NONE',  ( -2.024999999999999911, 45.00000000000000000, -27.00000000000000000 ) ) ;
#18325=EDGE_LOOP ( 'NONE', ( #11237, #18207 ) ) ;
#18327=VECTOR ( 'NONE', #6609, 1000.000000000000000 ) ;
#18334=DIRECTION ( 'NONE',  ( 0.000000000000000000, 0.000000000000000000, 1.000000000000000000 ) ) ;
#18343=ORIENTED_EDGE ( 'NONE', *, *, #6530, .T. ) ;
#18354=AXIS2_PLACEMENT_3D ( 'NONE', #23021, #3021, #17409 ) ;
#18358=CIRCLE ( 'NONE', #19143, 11.00000000000000000 ) ;
#18369=ORIENTED_EDGE ( 'NONE', *, *, #18944, .F. ) ;
#18375=ADVANCED_FACE ( 'NONE', ( #11903 ), #19007, .T. ) ;
#18376=CIRCLE ( 'NONE', #5533, 50.00000000000000000 ) ;
#18416=AXIS2_PLACEMENT_3D ( 'NONE', #10761, #1272, #3338 ) ;
#18419=DIRECTION ( 'NONE',  ( 1.000000000000000000, 0.000000000000000000, 0.000000000000000000 ) ) ;
#18421=DIRECTION ( 'NONE',  ( 0.000000000000000000, 0.000000000000000000, 1.000000000000000000 ) ) ;
#18436=CARTESIAN_POINT ( 'NONE',  ( -40.99749999999999517, 0.000000000000000000, 0.000000000000000000 ) ) ;
#18444=VERTEX_POINT ( 'NONE', #23156 ) ;
#18452=AXIS2_PLACEMENT_3D ( 'NONE', #1919, #2162, #13507 ) ;
#18466=VERTEX_POINT ( 'NONE', #3125 ) ;
#18479=CARTESIAN_POINT ( 'NONE',  ( 40.99749999999998096, 6.781874047275040887E-15, 9.499999999999989342 ) ) ;
#18489=AXIS2_PLACEMENT_3D ( 'NONE', #10750, #22130, #23818 ) ;
#18494=EDGE_CURVE ( 'NONE', #6052, #19513, #4735, .T. ) ;
#18501=DIRECTION ( 'NONE',  ( -1.000000000000000000, 0.000000000000000000, 0.000000000000000000 ) ) ;
#18507=DIRECTION ( 'NONE',  ( -0.000000000000000000, -0.000000000000000000, -1.000000000000000000 ) ) ;
#18511=CARTESIAN_POINT ( 'NONE',  ( 40.99749999999998096, 5.618459588085056979E-15, 0.000000000000000000 ) ) ;
#18512=ORIENTED_EDGE ( 'NONE', *, *, #4031, .F. ) ;
#18518=DIRECTION ( 'NONE',  ( -0.000000000000000000, -0.000000000000000000, -1.000000000000000000 ) ) ;
#18520=VECTOR ( 'NONE', #15694, 1000.000000000000000 ) ;
#18527=VERTEX_POINT ( 'NONE', #8730 ) ;
#18554=VECTOR ( 'NONE', #23324, 1000.000000000000000 ) ;
#18559=ORIENTED_EDGE ( 'NONE', *, *, #19102, .T. ) ;
#18577=FACE_OUTER_BOUND ( 'NONE', #6365, .T. ) ;
#18584=EDGE_CURVE ( 'NONE', #23464, #18617, #16148, .T. ) ;
#18612=VERTEX_POINT ( 'NONE', #23830 ) ;
#18617=VERTEX_POINT ( 'NONE', #16502 ) ;
#18621=LINE ( 'NONE', #10903, #5646 ) ;
#18627=CARTESIAN_POINT ( 'NONE',  ( -28.99999999999999645, -29.50000000000001066, -27.00000000000000000 ) ) ;
#18630=ORIENTED_EDGE ( 'NONE', *, *, #20336, .T. ) ;
#18631=ADVANCED_FACE ( 'NONE', ( #12363 ), #23959, .T. ) ;
#18635=CARTESIAN_POINT ( 'NONE',  ( -39.99999999999999289, 29.50000000000000000, 27.00000000000000000 ) ) ;
#18640=EDGE_CURVE ( 'NONE', #16505, #15077, #16028, .T. ) ;
#18641=AXIS2_PLACEMENT_3D ( 'NONE', #11349, #15035, #16864 ) ;
#18652=PLANE ( 'NONE',  #2934 ) ;
#18661=DIRECTION ( 'NONE',  ( -0.000000000000000000, -0.000000000000000000, -1.000000000000000000 ) ) ;
#18662=DIRECTION ( 'NONE',  ( -4.613626265895763066E-16, -1.000000000000000000, 0.000000000000000000 ) ) ;
#18663=CARTESIAN_POINT ( 'NONE',  ( -16.99687406587156602, 7.923972684219727114, -5.245599057861380032 ) ) ;
#18671=DIRECTION ( 'NONE',  ( -1.000000000000000000, 0.000000000000000000, 0.000000000000000000 ) ) ;
#18681=DIRECTION ( 'NONE',  ( -0.000000000000000000, -0.000000000000000000, -1.000000000000000000 ) ) ;
#18687=FACE_OUTER_BOUND ( 'NONE', #9379, .T. ) ;
#18703=ORIENTED_EDGE ( 'NONE', *, *, #11974, .T. ) ;
#18726=ADVANCED_FACE ( 'NONE', ( #12324 ), #6845, .T. ) ;
#18737=EDGE_CURVE ( 'NONE', #13688, #588, #14041, .T. ) ;
#18739=DIRECTION ( 'NONE',  ( 0.000000000000000000, 0.000000000000000000, 1.000000000000000000 ) ) ;
#18740=ORIENTED_EDGE ( 'NONE', *, *, #9148, .F. ) ;
#18752=EDGE_LOOP ( 'NONE', ( #3489, #7076, #17814, #2282 ) ) ;
#18769=CARTESIAN_POINT ( 'NONE',  ( -16.82499651802898200, 7.532250541895348483, 5.808290850931494553 ) ) ;
#18773=ORIENTED_EDGE ( 'NONE', *, *, #19488, .T. ) ;
#18776=DIRECTION ( 'NONE',  ( 1.000000000000000000, 0.000000000000000000, 0.000000000000000000 ) ) ;
#18777=EDGE_CURVE ( 'NONE', #2222, #2505, #57, .T. ) ;
#18791=CIRCLE ( 'NONE', #8261, 1.500000000000001332 ) ;
#18799=CARTESIAN_POINT ( 'NONE',  ( 40.00000000000000000, -27.79189783386526358, 27.00000000000000000 ) ) ;
#18810=AXIS2_PLACEMENT_3D ( 'NONE', #5620, #11078, #18776 ) ;
#18820=VERTEX_POINT ( 'NONE', #1588 ) ;
#18824=AXIS2_PLACEMENT_3D ( 'NONE', #13533, #11670, #2786 ) ;
#18826=VECTOR ( 'NONE', #5680, 1000.000000000000000 ) ;
#18832=VECTOR ( 'NONE', #854, 1000.000000000000114 ) ;
#18833=ORIENTED_EDGE ( 'NONE', *, *, #7253, .F. ) ;
#18837=DIRECTION ( 'NONE',  ( 0.000000000000000000, 0.000000000000000000, 1.000000000000000000 ) ) ;
#18855=VECTOR ( 'NONE', #23309, 1000.000000000000000 ) ;
#18868=VERTEX_POINT ( 'NONE', #16338 ) ;
#18873=DIRECTION ( 'NONE',  ( -0.000000000000000000, 0.000000000000000000, -1.000000000000000000 ) ) ;
#18874=CARTESIAN_POINT ( 'NONE',  ( 1.999999999999994449, -45.00000000000000000, -27.00000000000000000 ) ) ;
#18876=CIRCLE ( 'NONE', #15772, 1.999999999999994449 ) ;
#18880=ORIENTED_EDGE ( 'NONE', *, *, #4708, .F. ) ;
#18881=ORIENTED_EDGE ( 'NONE', *, *, #476, .T. ) ;
#18894=DIRECTION ( 'NONE',  ( 1.000000000000000000, 0.000000000000000000, 0.000000000000000000 ) ) ;
#18897=CARTESIAN_POINT ( 'NONE',  ( -40.89823313241237912, -26.41789760203349502, 27.00000000000000000 ) ) ;
#18898=AXIS2_PLACEMENT_3D ( 'NONE', #4132, #11911, #20710 ) ;
#18900=VERTEX_POINT ( 'NONE', #22810 ) ;
#18919=CIRCLE ( 'NONE', #21257, 18.50000000000000000 ) ;
#18920=EDGE_CURVE ( 'NONE', #7541, #2619, #355, .T. ) ;
#18925=DIRECTION ( 'NONE',  ( -4.613626265895764052E-16, 1.000000000000000000, 0.000000000000000000 ) ) ;
#18929=DIRECTION ( 'NONE',  ( -0.000000000000000000, -0.000000000000000000, -1.000000000000000000 ) ) ;
#18935=FACE_BOUND ( 'NONE', #15672, .T. ) ;
#18936=DIRECTION ( 'NONE',  ( 0.000000000000000000, 0.000000000000000000, 1.000000000000000000 ) ) ;
#18944=EDGE_CURVE ( 'NONE', #14507, #2676, #9383, .T. ) ;
#18954=ORIENTED_EDGE ( 'NONE', *, *, #10147, .T. ) ;
#18960=ORIENTED_EDGE ( 'NONE', *, *, #12494, .T. ) ;
#18978=ORIENTED_EDGE ( 'NONE', *, *, #9876, .F. ) ;
#18979=VECTOR ( 'NONE', #23840, 1000.000000000000000 ) ;
#18993=DIRECTION ( 'NONE',  ( 1.000000000000000000, -0.000000000000000000, -0.000000000000000000 ) ) ;
#18994=DIRECTION ( 'NONE',  ( -0.000000000000000000, -0.000000000000000000, 1.000000000000000000 ) ) ;
#18996=ORIENTED_EDGE ( 'NONE', *, *, #12137, .F. ) ;
#18997=DIRECTION ( 'NONE',  ( 1.000000000000000000, 0.000000000000000000, 0.000000000000000000 ) ) ;
#19007=CYLINDRICAL_SURFACE ( 'NONE', #16765, 11.00000000000000355 ) ;
#19016=AXIS2_PLACEMENT_3D ( 'NONE', #5807, #13233, #10802 ) ;
#19019=CYLINDRICAL_SURFACE ( 'NONE', #23155, 5.100000000000000533 ) ;
#19052=DIRECTION ( 'NONE',  ( -0.000000000000000000, -0.000000000000000000, -1.000000000000000000 ) ) ;
#19072=VECTOR ( 'NONE', #2287, 1000.000000000000000 ) ;
#19077=CARTESIAN_POINT ( 'NONE',  ( -39.99999999999999289, 27.79189783386526358, 27.00000000000000000 ) ) ;
#19082=DIRECTION ( 'NONE',  ( -0.000000000000000000, -0.000000000000000000, -1.000000000000000000 ) ) ;
#19084=CARTESIAN_POINT ( 'NONE',  ( -14.51962751333974211, 3.765689428759028790, -8.721787840009202597 ) ) ;
#19086=CARTESIAN_POINT ( 'NONE',  ( 23.84999999999999432, -15.03999999999999559, 25.00000000000000000 ) ) ;
#19093=AXIS2_PLACEMENT_3D ( 'NONE', #15878, #14279, #8428 ) ;
#19099=EDGE_CURVE ( 'NONE', #18612, #23407, #9785, .T. ) ;
#19102=EDGE_CURVE ( 'NONE', #4529, #16505, #21080, .T. ) ;
#19103=ORIENTED_EDGE ( 'NONE', *, *, #7733, .T. ) ;
#19104=DIRECTION ( 'NONE',  ( 0.000000000000000000, 0.000000000000000000, 1.000000000000000000 ) ) ;
#19109=ORIENTED_EDGE ( 'NONE', *, *, #22907, .F. ) ;
#19110=FACE_OUTER_BOUND ( 'NONE', #6724, .T. ) ;
#19114=DIRECTION ( 'NONE',  ( -0.000000000000000000, -0.000000000000000000, 1.000000000000000000 ) ) ;
#19115=DIRECTION ( 'NONE',  ( -0.000000000000000000, -0.000000000000000000, -1.000000000000000000 ) ) ;
#19120=VERTEX_POINT ( 'NONE', #21344 ) ;
#19141=ORIENTED_EDGE ( 'NONE', *, *, #3175, .T. ) ;
#19143=AXIS2_PLACEMENT_3D ( 'NONE', #1678, #3392, #22071 ) ;
#19148=ORIENTED_EDGE ( 'NONE', *, *, #21599, .T. ) ;
#19149=EDGE_CURVE ( 'NONE', #10247, #14507, #11792, .T. ) ;
#19152=CARTESIAN_POINT ( 'NONE',  ( 41.99999999999999289, 5.618459588085056979E-15, 0.000000000000000000 ) ) ;
#19167=CARTESIAN_POINT ( 'NONE',  ( 0.000000000000000000, -15.23000000000000220, 27.00000000000000000 ) ) ;
#19171=EDGE_CURVE ( 'NONE', #17527, #2222, #12410, .T. ) ;
#19173=AXIS2_PLACEMENT_3D ( 'NONE', #11183, #7656, #13265 ) ;
#19176=LINE ( 'NONE', #516, #28 ) ;
#19207=DIRECTION ( 'NONE',  ( 1.000000000000000000, 0.000000000000000000, 0.000000000000000000 ) ) ;
#19240=AXIS2_PLACEMENT_3D ( 'NONE', #2745, #925, #4709 ) ;
#19242=CARTESIAN_POINT ( 'NONE',  ( 0.000000000000000000, 15.03999999999999915, -25.00000000000000000 ) ) ;
#19244=VECTOR ( 'NONE', #17116, 1000.000000000000000 ) ;
#19254=CARTESIAN_POINT ( 'NONE',  ( 41.99999999999999289, 25.93535998569253920, 27.00000000000000000 ) ) ;
#19255=DIRECTION ( 'NONE',  ( -1.000000000000000000, 0.000000000000000000, 0.000000000000000000 ) ) ;
#19260=FACE_OUTER_BOUND ( 'NONE', #3838, .T. ) ;
#19267=LINE ( 'NONE', #22929, #5658 ) ;
#19270=FACE_OUTER_BOUND ( 'NONE', #3417, .T. ) ;
#19277=ORIENTED_EDGE ( 'NONE', *, *, #6902, .F. ) ;
#19286=CARTESIAN_POINT ( 'NONE',  ( 40.89823313241238623, -26.41789760203348081, 27.00000000000000000 ) ) ;
#19298=ADVANCED_FACE ( 'NONE', ( #14599 ), #3144, .T. ) ;
#19302=EDGE_CURVE ( 'NONE', #15047, #16347, #12512, .T. ) ;
#19303=CARTESIAN_POINT ( 'NONE',  ( 39.99999999999999289, 27.79189783386526358, 27.00000000000000000 ) ) ;
#19305=VECTOR ( 'NONE', #1241, 1000.000000000000000 ) ;
#19307=ORIENTED_EDGE ( 'NONE', *, *, #20420, .F. ) ;
#19312=CARTESIAN_POINT ( 'NONE',  ( 0.000000000000000000, -15.03999999999999915, 25.00000000000000000 ) ) ;
#19315=APPLICATION_CONTEXT ( 'automotive_design' ) ;
#19321=CIRCLE ( 'NONE', #6852, 10.50249999999999950 ) ;
#19328=ORIENTED_EDGE ( 'NONE', *, *, #14687, .F. ) ;
#19336=EDGE_CURVE ( 'NONE', #12319, #6874, #10200, .T. ) ;
#19344=CYLINDRICAL_SURFACE ( 'NONE', #12981, 14.99999999999999822 ) ;
#19352=ORIENTED_EDGE ( 'NONE', *, *, #16258, .T. ) ;
#19362=DIRECTION ( 'NONE',  ( 1.000000000000000000, 0.000000000000000000, 0.000000000000000000 ) ) ;
#19366=LINE ( 'NONE', #21673, #20775 ) ;
#19369=DIRECTION ( 'NONE',  ( 1.000000000000000000, 0.000000000000000000, 0.000000000000000000 ) ) ;
#19372=CARTESIAN_POINT ( 'NONE',  ( 16.68617496892349905, -7.233372502334337817, 6.175747996014750996 ) ) ;
#19373=DIRECTION ( 'NONE',  ( -1.000000000000000000, 0.000000000000000000, 0.000000000000000000 ) ) ;
#19379=VERTEX_POINT ( 'NONE', #13502 ) ;
#19381=DIRECTION ( 'NONE',  ( 0.000000000000000000, 0.000000000000000000, 1.000000000000000000 ) ) ;
#19389=ORIENTED_EDGE ( 'NONE', *, *, #9756, .T. ) ;
#19392=CARTESIAN_POINT ( 'NONE',  ( 0.000000000000000000, 45.00000000000000000, -23.99999999999999645 ) ) ;
#19395=CARTESIAN_POINT ( 'NONE',  ( 0.000000000000000000, -45.00000000000000000, -27.00000000000000000 ) ) ;
#19397=CARTESIAN_POINT ( 'NONE',  ( 0.000000000000000000, -45.00000000000000000, 27.00000000000000000 ) ) ;
#19401=ORIENTED_EDGE ( 'NONE', *, *, #4266, .F. ) ;
#19404=VERTEX_POINT ( 'NONE', #7628 ) ;
#19407=DIRECTION ( 'NONE',  ( -0.000000000000000000, -0.000000000000000000, -1.000000000000000000 ) ) ;
#19410=CARTESIAN_POINT ( 'NONE',  ( 15.00000000000000355, -0.3238088414458117903, -9.499999999999987566 ) ) ;
#19440=EDGE_CURVE ( 'NONE', #13688, #22991, #12153, .T. ) ;
#19445=ORIENTED_EDGE ( 'NONE', *, *, #12348, .F. ) ;
#19449=FACE_OUTER_BOUND ( 'NONE', #20209, .T. ) ;
#19464=EDGE_CURVE ( 'NONE', #678, #6052, #15442, .T. ) ;
#19469=CARTESIAN_POINT ( 'NONE',  ( -14.99999999999999822, 6.045577542124163753E-21, -9.499999999999994671 ) ) ;
#19470=DIRECTION ( 'NONE',  ( -0.9160001545545232160, 0.4011779117250717785, 0.000000000000000000 ) ) ;
#19472=CARTESIAN_POINT ( 'NONE',  ( -17.15242344757784210, -8.297343789534776803, 4.632629386303505292 ) ) ;
#19474=AXIS2_PLACEMENT_3D ( 'NONE', #15669, #11890, #17624 ) ;
#19481=DIRECTION ( 'NONE',  ( -0.000000000000000000, -0.000000000000000000, -1.000000000000000000 ) ) ;
#19483=CARTESIAN_POINT ( 'NONE',  ( 16.08510323282434484, -6.088885580147184839, -7.295537496892074536 ) ) ;
#19484=AXIS2_PLACEMENT_3D ( 'NONE', #16283, #14438, #23745 ) ;
#19487=CARTESIAN_POINT ( 'NONE',  ( 29.00000000000000711, -29.50000000000000711, 27.00000000000000000 ) ) ;
#19488=EDGE_CURVE ( 'NONE', #5422, #732, #4684, .T. ) ;
#19493=DIRECTION ( 'NONE',  ( -0.000000000000000000, -0.000000000000000000, -1.000000000000000000 ) ) ;
#19495=EDGE_CURVE ( 'NONE', #2222, #721, #2881, .T. ) ;
#19505=CARTESIAN_POINT ( 'NONE',  ( 0.000000000000000000, -45.00000000000000000, 27.00000000000000000 ) ) ;
#19509=CARTESIAN_POINT ( 'NONE',  ( 40.00000000000000000, -27.79189783386526358, -27.00000000000000000 ) ) ;
#19513=VERTEX_POINT ( 'NONE', #1066 ) ;
#19519=ORIENTED_EDGE ( 'NONE', *, *, #6077, .F. ) ;
#19529=VERTEX_POINT ( 'NONE', #570 ) ;
#19536=DIRECTION ( 'NONE',  ( -0.000000000000000000, -0.000000000000000000, -1.000000000000000000 ) ) ;
#19539=EDGE_LOOP ( 'NONE', ( #10297, #8052, #6951, #1147 ) ) ;
#19550=EDGE_CURVE ( 'NONE', #230, #15957, #15812, .T. ) ;
#19566=AXIS2_PLACEMENT_3D ( 'NONE', #9869, #18929, #2209 ) ;
#19570=PRODUCT ( 'Body', 'Body', '', ( #201 ) ) ;
#19575=VERTEX_POINT ( 'NONE', #699 ) ;
#19579=EDGE_CURVE ( 'NONE', #12687, #19120, #13619, .T. ) ;
#19582=ORIENTED_EDGE ( 'NONE', *, *, #16741, .F. ) ;
#19588=VECTOR ( 'NONE', #23088, 1000.000000000000000 ) ;
#19596=CARTESIAN_POINT ( 'NONE',  ( 20.85000000000000853, 15.03999999999999915, 25.00000000000000000 ) ) ;
#19604=EDGE_CURVE ( 'NONE', #569, #5416, #3103, .T. ) ;
#19612=ADVANCED_FACE ( 'NONE', ( #10540 ), #3360, .F. ) ;
#19618=ORIENTED_EDGE ( 'NONE', *, *, #7804, .T. ) ;
#19624=ORIENTED_EDGE ( 'NONE', *, *, #13931, .T. ) ;
#19625=DIRECTION ( 'NONE',  ( 1.000000000000000000, 0.000000000000000000, 0.000000000000000000 ) ) ;
#19629=AXIS2_PLACEMENT_3D ( 'NONE', #382, #1958, #22032 ) ;
#19633=EDGE_LOOP ( 'NONE', ( #11097, #14395, #21312, #5061, #16734, #19277 ) ) ;
#19635=DIRECTION ( 'NONE',  ( -0.000000000000000000, -0.000000000000000000, 1.000000000000000000 ) ) ;
#19643=CARTESIAN_POINT ( 'NONE',  ( 0.000000000000000000, 15.03999999999999915, 27.00000000000000000 ) ) ;
#19648=ADVANCED_FACE ( 'NONE', ( #12382 ), #1297, .F. ) ;
#19649=VERTEX_POINT ( 'NONE', #12742 ) ;
#19651=VECTOR ( 'NONE', #16106, 1000.000000000000000 ) ;
#19654=ORIENTED_EDGE ( 'NONE', *, *, #11803, .T. ) ;
#19655=VECTOR ( 'NONE', #2075, 1000.000000000000000 ) ;
#19661=CONICAL_SURFACE ( 'NONE', #7166, 1.999999999999994449, 1.029744258676653201 ) ;
#19666=EDGE_CURVE ( 'NONE', #21154, #18241, #4973, .T. ) ;
#19671=LINE ( 'NONE', #6963, #19651 ) ;
#19680=ORIENTED_EDGE ( 'NONE', *, *, #18737, .F. ) ;
#19690=DIRECTION ( 'NONE',  ( -0.000000000000000000, -0.000000000000000000, -1.000000000000000000 ) ) ;
#19693=AXIS2_PLACEMENT_3D ( 'NONE', #17055, #354, #7766 ) ;
#19697=EDGE_LOOP ( 'NONE', ( #12568, #17408, #14594, #2095 ) ) ;
#19699=VECTOR ( 'NONE', #9093, 1000.000000000000000 ) ;
#19708=ORIENTED_EDGE ( 'NONE', *, *, #9297, .F. ) ;
#19724=EDGE_CURVE ( 'NONE', #14, #5201, #3013, .T. ) ;
#19737=CARTESIAN_POINT ( 'NONE',  ( -14.51962751333974033, -3.765689428759031010, 8.721787840009202597 ) ) ;
#19757=CARTESIAN_POINT ( 'NONE',  ( 14.51962751333974389, 3.765689428759029234, 8.721787840009197268 ) ) ;
#19758=DIRECTION ( 'NONE',  ( 4.613626265895763066E-16, 1.000000000000000000, 0.000000000000000000 ) ) ;
#19762=DIRECTION ( 'NONE',  ( -1.000000000000000000, 0.000000000000000000, 0.000000000000000000 ) ) ;
#19764=DIRECTION ( 'NONE',  ( 1.000000000000000000, 0.000000000000000000, 0.000000000000000000 ) ) ;
#19773=ORIENTED_EDGE ( 'NONE', *, *, #19550, .T. ) ;
#19780=CARTESIAN_POINT ( 'NONE',  ( -40.89823313241237912, -26.41789760203349502, 27.00000000000000000 ) ) ;
#19782=ORIENTED_EDGE ( 'NONE', *, *, #18150, .F. ) ;
#19811=EDGE_CURVE ( 'NONE', #11194, #12687, #5832, .T. ) ;
#19813=VECTOR ( 'NONE', #4686, 1000.000000000000000 ) ;
#19820=ORIENTED_EDGE ( 'NONE', *, *, #19099, .F. ) ;
#19821=CARTESIAN_POINT ( 'NONE',  ( 40.89823313241237912, 26.41789760203348081, 27.00000000000000000 ) ) ;
#19824=ORIENTED_EDGE ( 'NONE', *, *, #17211, .F. ) ;
#19828=AXIS2_PLACEMENT_3D ( 'NONE', #18627, #13234, #16772 ) ;
#19839=CARTESIAN_POINT ( 'NONE',  ( -16.68617496892349905, -7.233372502334341370, -6.175747996014760766 ) ) ;
#19843=LINE ( 'NONE', #19950, #16198 ) ;
#19845=DIRECTION ( 'NONE',  ( -0.000000000000000000, -0.000000000000000000, -1.000000000000000000 ) ) ;
#19847=CARTESIAN_POINT ( 'NONE',  ( -41.99999999999999289, 25.93535998569253920, 27.00000000000000000 ) ) ;
#19848=CARTESIAN_POINT ( 'NONE',  ( 16.99687406587155891, -7.923972684219720009, -5.245599057861367598 ) ) ;
#19855=EDGE_CURVE ( 'NONE', #13001, #7696, #10112, .T. ) ;
#19857=DIRECTION ( 'NONE',  ( -1.000000000000000000, 0.000000000000000000, 0.000000000000000000 ) ) ;
#19865=VERTEX_POINT ( 'NONE', #4417 ) ;
#19868=DIRECTION ( 'NONE',  ( 0.000000000000000000, 0.000000000000000000, 1.000000000000000000 ) ) ;
#19872=FACE_BOUND ( 'NONE', #4906, .T. ) ;
#19879=EDGE_LOOP ( 'NONE', ( #3569, #7756, #17993, #12843 ) ) ;
#19883=EDGE_CURVE ( 'NONE', #9464, #569, #6358, .T. ) ;
#19885=DIRECTION ( 'NONE',  ( -1.000000000000000000, -0.000000000000000000, -0.000000000000000000 ) ) ;
#19886=AXIS2_PLACEMENT_3D ( 'NONE', #2449, #18936, #6118 ) ;
#19895=FACE_OUTER_BOUND ( 'NONE', #5324, .T. ) ;
#19898=LINE ( 'NONE', #23207, #8122 ) ;
#19899=ADVANCED_FACE ( 'NONE', ( #17565 ), #10489, .F. ) ;
#19907=CARTESIAN_POINT ( 'NONE',  ( -2.024999999999999911, -45.00000000000000000, -27.00000000000000000 ) ) ;
#19913=CARTESIAN_POINT ( 'NONE',  ( 14.51962751333974389, 3.765689428759029234, 27.00000000000000000 ) ) ;
#19918=LINE ( 'NONE', #10264, #20084 ) ;
#19923=CARTESIAN_POINT ( 'NONE',  ( 0.000000000000000000, -15.03999999999999915, 27.00000000000000000 ) ) ;
#19927=CARTESIAN_POINT ( 'NONE',  ( -23.85000000000000497, 15.03999999999999915, 27.00000000000000000 ) ) ;
#19929=ORIENTED_EDGE ( 'NONE', *, *, #15324, .F. ) ;
#19940=DIRECTION ( 'NONE',  ( -0.000000000000000000, -0.000000000000000000, -1.000000000000000000 ) ) ;
#19941=ORIENTED_EDGE ( 'NONE', *, *, #3499, .T. ) ;
#19950=CARTESIAN_POINT ( 'NONE',  ( -41.99999999999999289, 1.163414459189984894E-15, -9.499999999999994671 ) ) ;
#19958=EDGE_CURVE ( 'NONE', #5616, #16538, #1002, .T. ) ;
#19988=CARTESIAN_POINT ( 'NONE',  ( 15.09475045435787877, 4.494086555308248521, 8.407297576120603466 ) ) ;
#20027=VERTEX_POINT ( 'NONE', #11955 ) ;
#20029=AXIS2_PLACEMENT_3D ( 'NONE', #15629, #21277, #6632 ) ;
#20034=CIRCLE ( 'NONE', #1722, 4.999999999999997335 ) ;
#20036=CARTESIAN_POINT ( 'NONE',  ( 41.49999999999999289, 27.79189783386526358, -27.00000000000000000 ) ) ;
#20039=DIRECTION ( 'NONE',  ( 0.000000000000000000, 0.000000000000000000, 1.000000000000000000 ) ) ;
#20048=LINE ( 'NONE', #21997, #16530 ) ;
#20066=EDGE_CURVE ( 'NONE', #18527, #20316, #23398, .T. ) ;
#20072=DIRECTION ( 'NONE',  ( 0.000000000000000000, 0.000000000000000000, 1.000000000000000000 ) ) ;
#20079=ORIENTED_EDGE ( 'NONE', *, *, #17791, .T. ) ;
#20083=DIRECTION ( 'NONE',  ( -0.000000000000000000, -0.000000000000000000, -1.000000000000000000 ) ) ;
#20084=VECTOR ( 'NONE', #19690, 1000.000000000000000 ) ;
#20089=CARTESIAN_POINT ( 'NONE',  ( -14.51962751333974211, 3.765689428759028790, -8.721787840009202597 ) ) ;
#20108=DIRECTION ( 'NONE',  ( -1.000000000000000000, 0.000000000000000000, 0.000000000000000000 ) ) ;
#20118=CARTESIAN_POINT ( 'NONE',  ( 17.49066032632880763, 9.200828712690864108, 2.414248458042549839 ) ) ;
#20120=VERTEX_POINT ( 'NONE', #12682 ) ;
#20129=CARTESIAN_POINT ( 'NONE',  ( 0.000000000000000000, -15.03999999999999915, 25.00000000000000000 ) ) ;
#20131=VERTEX_POINT ( 'NONE', #7414 ) ;
#20134=DIRECTION ( 'NONE',  ( -0.4011779117250717785, 0.9160001545545232160, 0.000000000000000000 ) ) ;
#20137=CARTESIAN_POINT ( 'NONE',  ( 40.89823313241237912, 26.41789760203348081, -27.00000000000000000 ) ) ;
#20176=CARTESIAN_POINT ( 'NONE',  ( 15.00000000000000000, 6.781880092842756171E-15, 9.499999999999987566 ) ) ;
#20189=CARTESIAN_POINT ( 'NONE',  ( 40.89823313241238623, -26.41789760203348081, -27.00000000000000000 ) ) ;
#20190=DIRECTION ( 'NONE',  ( -1.000000000000000000, 0.000000000000000000, 0.000000000000000000 ) ) ;
#20202=CARTESIAN_POINT ( 'NONE',  ( 15.07341617659253963, -4.495283618570416806, 8.379779594489201955 ) ) ;
#20209=EDGE_LOOP ( 'NONE', ( #9272, #16692, #21638, #3551 ) ) ;
#20227=CARTESIAN_POINT ( 'NONE',  ( 20.85000000000000853, 15.03999999999999915, 25.00000000000000000 ) ) ;
#20230=CARTESIAN_POINT ( 'NONE',  ( 17.59008829125738416, 9.499485695642613692, 0.4958780962348190990 ) ) ;
#20244=ORIENTED_EDGE ( 'NONE', *, *, #14548, .F. ) ;
#20253=DIRECTION ( 'NONE',  ( -0.000000000000000000, -0.000000000000000000, -1.000000000000000000 ) ) ;
#20256=FACE_OUTER_BOUND ( 'NONE', #10081, .T. ) ;
#20261=CARTESIAN_POINT ( 'NONE',  ( 2.024999999999999911, -45.00000000000000000, 27.00000000000000000 ) ) ;
#20266=DIRECTION ( 'NONE',  ( -0.000000000000000000, -0.000000000000000000, -1.000000000000000000 ) ) ;
#20279=FACE_OUTER_BOUND ( 'NONE', #17509, .T. ) ;
#20285=CYLINDRICAL_SURFACE ( 'NONE', #14165, 15.00000000000000000 ) ;
#20287=DIRECTION ( 'NONE',  ( -0.000000000000000000, -0.000000000000000000, -1.000000000000000000 ) ) ;
#20300=ORIENTED_EDGE ( 'NONE', *, *, #4493, .F. ) ;
#20316=VERTEX_POINT ( 'NONE', #22814 ) ;
#20323=ORIENTED_EDGE ( 'NONE', *, *, #4708, .T. ) ;
#20331=DIRECTION ( 'NONE',  ( -1.000000000000000000, 0.000000000000000000, 0.000000000000000000 ) ) ;
#20333=DIRECTION ( 'NONE',  ( -1.000000000000000000, -1.337728473353585242E-16, 0.000000000000000000 ) ) ;
#20336=EDGE_CURVE ( 'NONE', #11923, #23352, #2789, .T. ) ;
#20347=EDGE_LOOP ( 'NONE', ( #19582, #3679, #17027, #17259 ) ) ;
#20355=CARTESIAN_POINT ( 'NONE',  ( 30.44534269664589843, 40.40463133211081015, 27.00000000000000000 ) ) ;
#20359=AXIS2_PLACEMENT_3D ( 'NONE', #1097, #10694, #1461 ) ;
#20370=CARTESIAN_POINT ( 'NONE',  ( -17.19784311473120653, 8.411123426659422364, -4.422670359120419725 ) ) ;
#20373=ORIENTED_EDGE ( 'NONE', *, *, #5084, .F. ) ;
#20376=LINE ( 'NONE', #1944, #9429 ) ;
#20388=ORIENTED_EDGE ( 'NONE', *, *, #19811, .T. ) ;
#20394=DIRECTION ( 'NONE',  ( -1.000000000000000000, 0.000000000000000000, 0.000000000000000000 ) ) ;
#20399=CARTESIAN_POINT ( 'NONE',  ( 0.000000000000000000, 0.000000000000000000, 27.00000000000000000 ) ) ;
#20408=ORIENTED_EDGE ( 'NONE', *, *, #10499, .F. ) ;
#20412=ADVANCED_FACE ( 'NONE', ( #12415 ), #2502, .F. ) ;
#20415=LINE ( 'NONE', #7454, #998 ) ;
#20420=EDGE_CURVE ( 'NONE', #17607, #2619, #17672, .T. ) ;
#20429=AXIS2_PLACEMENT_3D ( 'NONE', #2959, #8667, #6861 ) ;
#20439=ADVANCED_FACE ( 'NONE', ( #1213 ), #6586, .T. ) ;
#20444=ADVANCED_FACE ( 'NONE', ( #4756 ), #19661, .F. ) ;
#20451=VECTOR ( 'NONE', #12204, 1000.000000000000000 ) ;
#20452=ORIENTED_EDGE ( 'NONE', *, *, #14977, .T. ) ;
#20454=CARTESIAN_POINT ( 'NONE',  ( 0.000000000000000000, 15.23000000000000220, 27.00000000000000000 ) ) ;
#20458=DIRECTION ( 'NONE',  ( 4.613626265895764052E-16, -1.000000000000000000, 0.000000000000000000 ) ) ;
#20459=DIRECTION ( 'NONE',  ( 1.337728473353585242E-16, -1.000000000000000000, 0.000000000000000000 ) ) ;
#20461=CIRCLE ( 'NONE', #2540, 5.100000000000000533 ) ;
#20473=ORIENTED_EDGE ( 'NONE', *, *, #12704, .F. ) ;
#20482=FACE_OUTER_BOUND ( 'NONE', #4666, .T. ) ;
#20485=CIRCLE ( 'NONE', #11881, 1.999999999999994449 ) ;
#20490=LINE ( 'NONE', #3530, #15373 ) ;
#20494=CARTESIAN_POINT ( 'NONE',  ( -17.57831567727900790, 9.462949834988608089, 0.9681625741885162562 ) ) ;
#20496=( GEOMETRIC_REPRESENTATION_CONTEXT ( 3 ) GLOBAL_UNCERTAINTY_ASSIGNED_CONTEXT ( ( #8380 ) ) GLOBAL_UNIT_ASSIGNED_CONTEXT ( ( #7780, #9264, #22685 ) ) REPRESENTATION_CONTEXT ( 'NONE', 'WORKASPACE' ) );
#20550=ORIENTED_EDGE ( 'NONE', *, *, #21104, .F. ) ;
#20554=ORIENTED_EDGE ( 'NONE', *, *, #18228, .T. ) ;
#20555=CARTESIAN_POINT ( 'NONE',  ( 1.999999999999994449, 45.00000000000000000, -26.97499999999999432 ) ) ;
#20570=EDGE_CURVE ( 'NONE', #230, #17527, #21608, .T. ) ;
#20577=ORIENTED_EDGE ( 'NONE', *, *, #18920, .F. ) ;
#20578=DIRECTION ( 'NONE',  ( 4.613626265895764052E-16, 1.000000000000000000, -0.000000000000000000 ) ) ;
#20585=ORIENTED_EDGE ( 'NONE', *, *, #3479, .T. ) ;
#20588=PLANE ( 'NONE',  #10959 ) ;
#20592=CARTESIAN_POINT ( 'NONE',  ( -14.51962751333974389, 3.765689428759031010, 27.00000000000000000 ) ) ;
#20594=ORIENTED_EDGE ( 'NONE', *, *, #23362, .F. ) ;
#20608=ORIENTED_EDGE ( 'NONE', *, *, #8287, .F. ) ;
#20613=CARTESIAN_POINT ( 'NONE',  ( -16.18147534945000032, 6.260849737139246862, -7.148624562014530781 ) ) ;
#20621=DIRECTION ( 'NONE',  ( -0.000000000000000000, -0.000000000000000000, -1.000000000000000000 ) ) ;
#20625=CARTESIAN_POINT ( 'NONE',  ( -23.85000000000000497, 15.03999999999999915, -25.00000000000000000 ) ) ;
#20633=AXIS2_PLACEMENT_3D ( 'NONE', #18259, #12499, #19857 ) ;
#20635=CARTESIAN_POINT ( 'NONE',  ( 15.00000000000000000, 5.618453542512190434E-15, -9.499999999999987566 ) ) ;
#20636=VECTOR ( 'NONE', #19114, 1000.000000000000000 ) ;
#20639=EDGE_CURVE ( 'NONE', #20648, #13451, #7288, .T. ) ;
#20643=ORIENTED_EDGE ( 'NONE', *, *, #992, .T. ) ;
#20647=CARTESIAN_POINT ( 'NONE',  ( 0.000000000000000000, 15.23000000000000220, 27.00000000000000000 ) ) ;
#20648=VERTEX_POINT ( 'NONE', #7167 ) ;
#20657=EDGE_LOOP ( 'NONE', ( #15228, #3326 ) ) ;
#20666=CARTESIAN_POINT ( 'NONE',  ( -41.99999999999999289, 0.000000000000000000, 0.000000000000000000 ) ) ;
#20679=ORIENTED_EDGE ( 'NONE', *, *, #2761, .T. ) ;
#20696=CARTESIAN_POINT ( 'NONE',  ( 23.85000000000000497, 15.03999999999999915, -25.00000000000000000 ) ) ;
#20698=EDGE_CURVE ( 'NONE', #2350, #3850, #6814, .T. ) ;
#20705=VERTEX_POINT ( 'NONE', #17801 ) ;
#20710=DIRECTION ( 'NONE',  ( 1.000000000000000000, 0.000000000000000000, 0.000000000000000000 ) ) ;
#20740=CARTESIAN_POINT ( 'NONE',  ( 0.000000000000000000, -45.00000000000000000, -23.99999999999999645 ) ) ;
#20741=EDGE_CURVE ( 'NONE', #18900, #13451, #18876, .T. ) ;
#20743=AXIS2_PLACEMENT_3D ( 'NONE', #4081, #13835, #415 ) ;
#20745=CARTESIAN_POINT ( 'NONE',  ( -1.999999999999994449, 45.00000000000000000, 27.00000000000000000 ) ) ;
#20748=ORIENTED_EDGE ( 'NONE', *, *, #9297, .T. ) ;
#20752=CARTESIAN_POINT ( 'NONE',  ( -40.99749999999999517, 1.163414459189984894E-15, -9.499999999999994671 ) ) ;
#20753=FACE_BOUND ( 'NONE', #49, .T. ) ;
#20762=AXIS2_PLACEMENT_3D ( 'NONE', #17457, #13436, #4553 ) ;
#20764=ORIENTED_EDGE ( 'NONE', *, *, #19464, .F. ) ;
#20768=CYLINDRICAL_SURFACE ( 'NONE', #14873, 11.00000000000001066 ) ;
#20774=ORIENTED_EDGE ( 'NONE', *, *, #3122, .F. ) ;
#20775=VECTOR ( 'NONE', #4969, 1000.000000000000000 ) ;
#20778=CARTESIAN_POINT ( 'NONE',  ( 0.000000000000000000, 0.000000000000000000, 27.00000000000000000 ) ) ;
#20784=EDGE_LOOP ( 'NONE', ( #19680, #3500, #4210, #7654 ) ) ;
#20789=ORIENTED_EDGE ( 'NONE', *, *, #17791, .F. ) ;
#20790=ORIENTED_EDGE ( 'NONE', *, *, #20420, .T. ) ;
#20798=LINE ( 'NONE', #9668, #18826 ) ;
#20804=ORIENTED_EDGE ( 'NONE', *, *, #24009, .T. ) ;
#20813=ORIENTED_EDGE ( 'NONE', *, *, #7420, .F. ) ;
#20828=AXIS2_PLACEMENT_3D ( 'NONE', #2819, #13440, #392 ) ;
#20830=VECTOR ( 'NONE', #3579, 1000.000000000000000 ) ;
#20831=DIRECTION ( 'NONE',  ( -1.000000000000000000, 0.000000000000000000, 0.000000000000000000 ) ) ;
#20835=CARTESIAN_POINT ( 'NONE',  ( 16.68617496892350260, 7.233372502334339593, -6.175747996014759877 ) ) ;
#20845=EDGE_CURVE ( 'NONE', #2809, #11886, #10295, .T. ) ;
#20857=DIRECTION ( 'NONE',  ( -1.000000000000000000, 0.000000000000000000, 0.000000000000000000 ) ) ;
#20863=CARTESIAN_POINT ( 'NONE',  ( -41.99999999999999289, 25.93535998569253920, 27.00000000000000000 ) ) ;
#20869=CONICAL_SURFACE ( 'NONE', #13450, 1.999999999999994449, 1.029744258676653201 ) ;
#20872=AXIS2_PLACEMENT_3D ( 'NONE', #19152, #2199, #16954 ) ;
#20883=ORIENTED_EDGE ( 'NONE', *, *, #19724, .F. ) ;
#20887=ORIENTED_EDGE ( 'NONE', *, *, #18737, .T. ) ;
#20907=VECTOR ( 'NONE', #5234, 1000.000000000000000 ) ;
#20917=EDGE_LOOP ( 'NONE', ( #12727, #9283 ) ) ;
#20937=ORIENTED_EDGE ( 'NONE', *, *, #19099, .T. ) ;
#20945=DIRECTION ( 'NONE',  ( 1.000000000000000000, -0.000000000000000000, -0.000000000000000000 ) ) ;
#20963=ORIENTED_EDGE ( 'NONE', *, *, #11662, .T. ) ;
#20966=FACE_OUTER_BOUND ( 'NONE', #484, .T. ) ;
#20968=CARTESIAN_POINT ( 'NONE',  ( 20.84999999999999432, -15.04000000000000448, 27.00000000000000000 ) ) ;
#20976=CARTESIAN_POINT ( 'NONE',  ( -14.80736872429922890, 4.130115634539730074, 8.564444421911371563 ) ) ;
#20983=ORIENTED_EDGE ( 'NONE', *, *, #6282, .T. ) ;
#20997=VERTEX_POINT ( 'NONE', #7528 ) ;
#21002=CARTESIAN_POINT ( 'NONE',  ( 41.50000000000000000, -27.79189783386526358, 27.00000000000000000 ) ) ;
#21007=EDGE_CURVE ( 'NONE', #3277, #8063, #8894, .T. ) ;
#21043=EDGE_LOOP ( 'NONE', ( #2469, #2050, #7710, #10156, #15176, #5891, #14058, #6825, #8194, #5353, #10508, #22954, #1195, #6690, #14670, #11378, #20679, #12708, #23716, #20585, #12768, #17410, #8961, #5265 ) ) ;
#21044=ORIENTED_EDGE ( 'NONE', *, *, #21387, .T. ) ;
#21052=EDGE_CURVE ( 'NONE', #19404, #18868, #20490, .T. ) ;
#21058=DIRECTION ( 'NONE',  ( -0.000000000000000000, -0.000000000000000000, 1.000000000000000000 ) ) ;
#21060=FACE_OUTER_BOUND ( 'NONE', #24076, .T. ) ;
#21071=DIRECTION ( 'NONE',  ( -0.000000000000000000, -0.000000000000000000, -1.000000000000000000 ) ) ;
#21079=DIRECTION ( 'NONE',  ( 0.000000000000000000, 0.000000000000000000, 1.000000000000000000 ) ) ;
#21080=LINE ( 'NONE', #3040, #23468 ) ;
#21104=EDGE_CURVE ( 'NONE', #11994, #10631, #22020, .T. ) ;
#21107=ORIENTED_EDGE ( 'NONE', *, *, #21599, .F. ) ;
#21112=FACE_BOUND ( 'NONE', #12082, .T. ) ;
#21138=AXIS2_PLACEMENT_3D ( 'NONE', #21248, #10376, #999 ) ;
#21139=CARTESIAN_POINT ( 'NONE',  ( -2.024999999999999911, 45.00000000000000000, -27.00000000000000000 ) ) ;
#21154=VERTEX_POINT ( 'NONE', #11426 ) ;
#21157=CIRCLE ( 'NONE', #19629, 4.999999999999997335 ) ;
#21163=VECTOR ( 'NONE', #3869, 1000.000000000000000 ) ;
#21167=ORIENTED_EDGE ( 'NONE', *, *, #18640, .T. ) ;
#21174=LINE ( 'NONE', #2380, #11906 ) ;
#21179=PLANE ( 'NONE',  #615 ) ;
#21181=ORIENTED_EDGE ( 'NONE', *, *, #9088, .F. ) ;
#21191=EDGE_CURVE ( 'NONE', #15047, #3047, #19267, .T. ) ;
#21218=CARTESIAN_POINT ( 'NONE',  ( -15.56475192642548855, 5.220978644676156577, 7.947934502462945083 ) ) ;
#21227=EDGE_CURVE ( 'NONE', #16538, #2790, #10712, .T. ) ;
#21230=EDGE_LOOP ( 'NONE', ( #23025, #4223, #22250, #15475 ) ) ;
#21237=DIRECTION ( 'NONE',  ( -0.000000000000000000, -0.000000000000000000, -1.000000000000000000 ) ) ;
#21240=CARTESIAN_POINT ( 'NONE',  ( -20.85000000000000853, 15.04000000000000092, 25.00000000000000000 ) ) ;
#21248=CARTESIAN_POINT ( 'NONE',  ( 29.00000000000000711, -29.50000000000000711, 27.00000000000000000 ) ) ;
#21250=EDGE_CURVE ( 'NONE', #18466, #16505, #21630, .T. ) ;
#21255=DIRECTION ( 'NONE',  ( 1.000000000000000000, -0.000000000000000000, -0.000000000000000000 ) ) ;
#21257=AXIS2_PLACEMENT_3D ( 'NONE', #21848, #23921, #7069 ) ;
#21277=DIRECTION ( 'NONE',  ( 0.000000000000000000, 0.000000000000000000, 1.000000000000000000 ) ) ;
#21289=DIRECTION ( 'NONE',  ( -0.000000000000000000, -0.000000000000000000, -1.000000000000000000 ) ) ;
#21291=LINE ( 'NONE', #21655, #14263 ) ;
#21307=CONICAL_SURFACE ( 'NONE', #10757, 1.999999999999994449, 1.029744258676653201 ) ;
#21309=CARTESIAN_POINT ( 'NONE',  ( -17.52920230446416738, -9.315347328456301312, -1.925892650121553196 ) ) ;
#21311=FACE_OUTER_BOUND ( 'NONE', #17851, .T. ) ;
#21312=ORIENTED_EDGE ( 'NONE', *, *, #24038, .T. ) ;
#21322=AXIS2_PLACEMENT_3D ( 'NONE', #20036, #10501, #16351 ) ;
#21344=CARTESIAN_POINT ( 'NONE',  ( 14.51962751333974389, -3.765689428759035895, 27.00000000000000000 ) ) ;
#21346=CARTESIAN_POINT ( 'NONE',  ( -28.27483331787887266, 41.23752903419610760, 27.00000000000000000 ) ) ;
#21362=CARTESIAN_POINT ( 'NONE',  ( 14.91624121966758487, -1.615102390220943818, -9.367332145225617523 ) ) ;
#21363=DIRECTION ( 'NONE',  ( -0.000000000000000000, -0.000000000000000000, -1.000000000000000000 ) ) ;
#21373=CIRCLE ( 'NONE', #18249, 1.500000000000001332 ) ;
#21379=EDGE_LOOP ( 'NONE', ( #5456, #9167, #23215 ) ) ;
#21387=EDGE_CURVE ( 'NONE', #13548, #20120, #20461, .T. ) ;
#21396=AXIS2_PLACEMENT_3D ( 'NONE', #21002, #2216, #8049 ) ;
#21419=PLANE ( 'NONE',  #23100 ) ;
#21421=CARTESIAN_POINT ( 'NONE',  ( -17.57831567727900435, -9.462949834988608089, -0.9681625741885125924 ) ) ;
#21435=VECTOR ( 'NONE', #5073, 1000.000000000000000 ) ;
#21442=VERTEX_POINT ( 'NONE', #24050 ) ;
#21447=ORIENTED_EDGE ( 'NONE', *, *, #16845, .T. ) ;
#21451=AXIS2_PLACEMENT_3D ( 'NONE', #5256, #23919, #18421 ) ;
#21453=CARTESIAN_POINT ( 'NONE',  ( 23.85000000000000497, 15.03999999999999915, 25.00000000000000000 ) ) ;
#21473=FACE_OUTER_BOUND ( 'NONE', #20784, .T. ) ;
#21474=EDGE_CURVE ( 'NONE', #13696, #18444, #1001, .T. ) ;
#21486=CARTESIAN_POINT ( 'NONE',  ( 29.00000000000000355, 29.50000000000000000, -27.00000000000000000 ) ) ;
#21489=DIRECTION ( 'NONE',  ( -0.000000000000000000, -0.000000000000000000, -1.000000000000000000 ) ) ;
#21496=ADVANCED_FACE ( 'NONE', ( #5392 ), #20869, .F. ) ;
#21497=FACE_OUTER_BOUND ( 'NONE', #11100, .T. ) ;
#21498=LINE ( 'NONE', #23457, #19588 ) ;
#21504=ORIENTED_EDGE ( 'NONE', *, *, #16679, .T. ) ;
#21526=CARTESIAN_POINT ( 'NONE',  ( 31.10231664966676846, -45.36128193761570770, -27.00000000000000000 ) ) ;
#21529=B_SPLINE_CURVE_WITH_KNOTS ( 'NONE', 3,
 ( #21875, #14779, #22009, #12588, #5288, #9045, #12715, #20176 ),
 .UNSPECIFIED., .F., .F.,
 ( 4, 2, 2, 4 ),
 ( 0.000000000000000000, 0.001946159586596647381, 0.002919239379894971072, 0.003892319173193294762 ),
 .UNSPECIFIED. ) ;
#21540=VECTOR ( 'NONE', #13923, 1000.000000000000000 ) ;
#21544=CARTESIAN_POINT ( 'NONE',  ( -15.09475045435787699, -4.494086555308247632, 8.407297576120608795 ) ) ;
#21559=AXIS2_PLACEMENT_3D ( 'NONE', #20399, #3688, #1741 ) ;
#21570=ORIENTED_EDGE ( 'NONE', *, *, #19440, .T. ) ;
#21584=FACE_OUTER_BOUND ( 'NONE', #7616, .T. ) ;
#21595=ORIENTED_EDGE ( 'NONE', *, *, #16099, .F. ) ;
#21599=EDGE_CURVE ( 'NONE', #721, #5790, #16194, .T. ) ;
#21600=AXIS2_PLACEMENT_3D ( 'NONE', #5765, #4185, #15752 ) ;
#21608=CIRCLE ( 'NONE', #7547, 23.84999999999999432 ) ;
#21610=LINE ( 'NONE', #4903, #12929 ) ;
#21618=EDGE_LOOP ( 'NONE', ( #3063, #15870, #8438, #7389 ) ) ;
#21625=EDGE_CURVE ( 'NONE', #3887, #15590, #7671, .T. ) ;
#21630=LINE ( 'NONE', #15998, #2151 ) ;
#21638=ORIENTED_EDGE ( 'NONE', *, *, #7777, .T. ) ;
#21644=ADVANCED_FACE ( 'NONE', ( #4280 ), #2949, .F. ) ;
#21647=PLANE ( 'NONE',  #103 ) ;
#21648=DIRECTION ( 'NONE',  ( -0.000000000000000000, -0.000000000000000000, -1.000000000000000000 ) ) ;
#21649=ADVANCED_FACE ( 'NONE', ( #13281 ), #13166, .T. ) ;
#21655=CARTESIAN_POINT ( 'NONE',  ( 1.999999999999994449, -45.00000000000000000, -23.99999999999999645 ) ) ;
#21663=VERTEX_POINT ( 'NONE', #7783 ) ;
#21673=CARTESIAN_POINT ( 'NONE',  ( 42.00000000000000000, -25.93535998569253920, 27.00000000000000000 ) ) ;
#21680=VECTOR ( 'NONE', #1894, 1000.000000000000000 ) ;
#21681=CARTESIAN_POINT ( 'NONE',  ( -14.94777716362147935, -1.291632522116892501, 9.417361603030281358 ) ) ;
#21684=DIRECTION ( 'NONE',  ( -1.000000000000000000, 0.000000000000000000, 0.000000000000000000 ) ) ;
#21695=AXIS2_PLACEMENT_3D ( 'NONE', #20129, #5356, #3405 ) ;
#21704=EDGE_CURVE ( 'NONE', #11857, #3699, #3342, .T. ) ;
#21709=CYLINDRICAL_SURFACE ( 'NONE', #6732, 1.999999999999994449 ) ;
#21723=PLANE ( 'NONE',  #10393 ) ;
#21741=CARTESIAN_POINT ( 'NONE',  ( -14.99999999999999822, 0.3242076166095213541, 9.499999999999994671 ) ) ;
#21747=DIRECTION ( 'NONE',  ( -0.000000000000000000, -0.000000000000000000, -1.000000000000000000 ) ) ;
#21752=DIRECTION ( 'NONE',  ( 1.000000000000000000, 0.000000000000000000, 0.000000000000000000 ) ) ;
#21777=ORIENTED_EDGE ( 'NONE', *, *, #10655, .F. ) ;
#21809=DIRECTION ( 'NONE',  ( -0.000000000000000000, -0.000000000000000000, -1.000000000000000000 ) ) ;
#21828=DIRECTION ( 'NONE',  ( 0.000000000000000000, 0.000000000000000000, -1.000000000000000000 ) ) ;
#21831=DIRECTION ( 'NONE',  ( 0.000000000000000000, 0.000000000000000000, 1.000000000000000000 ) ) ;
#21839=DIRECTION ( 'NONE',  ( -1.000000000000000000, 4.613626265895764052E-16, 0.000000000000000000 ) ) ;
#21848=CARTESIAN_POINT ( 'NONE',  ( 0.000000000000000000, 15.23000000000000220, 27.00000000000000000 ) ) ;
#21849=ORIENTED_EDGE ( 'NONE', *, *, #7102, .F. ) ;
#21861=CARTESIAN_POINT ( 'NONE',  ( 41.99999999999999289, 5.618459588085056979E-15, 0.000000000000000000 ) ) ;
#21865=CARTESIAN_POINT ( 'NONE',  ( 23.85000000000000142, 15.03999999999999915, -27.00000000000000000 ) ) ;
#21868=ORIENTED_EDGE ( 'NONE', *, *, #22568, .F. ) ;
#21874=DIRECTION ( 'NONE',  ( 1.000000000000000000, 0.000000000000000000, 0.000000000000000000 ) ) ;
#21875=CARTESIAN_POINT ( 'NONE',  ( 14.51962751333974211, -3.765689428759034563, 8.721787840009190163 ) ) ;
#21905=CARTESIAN_POINT ( 'NONE',  ( -14.99999999999999467, 0.3238088414458165643, -9.499999999999996447 ) ) ;
#21912=EDGE_CURVE ( 'NONE', #14761, #18444, #21955, .T. ) ;
#21937=PLANE ( 'NONE',  #23940 ) ;
#21947=ORIENTED_EDGE ( 'NONE', *, *, #4738, .F. ) ;
#21950=ORIENTED_EDGE ( 'NONE', *, *, #10682, .T. ) ;
#21954=VECTOR ( 'NONE', #11271, 1000.000000000000000 ) ;
#21955=LINE ( 'NONE', #5242, #22079 ) ;
#21963=DIRECTION ( 'NONE',  ( -0.000000000000000000, -0.000000000000000000, -1.000000000000000000 ) ) ;
#21970=EDGE_CURVE ( 'NONE', #678, #21154, #14621, .T. ) ;
#21972=AXIS2_PLACEMENT_3D ( 'NONE', #10864, #18334, #16495 ) ;
#21983=ORIENTED_EDGE ( 'NONE', *, *, #6830, .F. ) ;
#21984=CARTESIAN_POINT ( 'NONE',  ( 14.51962751333974389, -3.765689428759035895, 27.00000000000000000 ) ) ;
#21995=CIRCLE ( 'NONE', #20429, 5.100000000000000533 ) ;
#21997=CARTESIAN_POINT ( 'NONE',  ( -39.99999999999999289, 27.79189783386526358, 27.00000000000000000 ) ) ;
#22008=DIRECTION ( 'NONE',  ( -1.000000000000000000, -0.000000000000000000, -0.000000000000000000 ) ) ;
#22009=CARTESIAN_POINT ( 'NONE',  ( 14.79187224938325151, -2.570168443617190324, 9.168425918763418281 ) ) ;
#22011=EDGE_LOOP ( 'NONE', ( #7442, #6045, #3447, #12809 ) ) ;
#22018=VECTOR ( 'NONE', #13133, 1000.000000000000000 ) ;
#22020=CIRCLE ( 'NONE', #14596, 18.49999999999999645 ) ;
#22032=DIRECTION ( 'NONE',  ( 1.000000000000000000, 0.000000000000000000, 0.000000000000000000 ) ) ;
#22036=ADVANCED_FACE ( 'NONE', ( #13386 ), #22315, .T. ) ;
#22044=LINE ( 'NONE', #3725, #12686 ) ;
#22047=VERTEX_POINT ( 'NONE', #459 ) ;
#22069=CARTESIAN_POINT ( 'NONE',  ( 0.000000000000000000, -15.03999999999999915, 25.00000000000000000 ) ) ;
#22071=DIRECTION ( 'NONE',  ( 1.000000000000000000, 0.000000000000000000, 0.000000000000000000 ) ) ;
#22079=VECTOR ( 'NONE', #16225, 1000.000000000000000 ) ;
#22098=DIRECTION ( 'NONE',  ( -1.000000000000000000, 0.000000000000000000, 0.000000000000000000 ) ) ;
#22106=DIRECTION ( 'NONE',  ( -0.000000000000000000, -0.000000000000000000, -1.000000000000000000 ) ) ;
#22119=PLANE ( 'NONE',  #10770 ) ;
#22125=EDGE_CURVE ( 'NONE', #12983, #128, #7615, .T. ) ;
#22130=DIRECTION ( 'NONE',  ( -0.000000000000000000, -0.000000000000000000, -1.000000000000000000 ) ) ;
#22131=DIRECTION ( 'NONE',  ( 0.000000000000000000, 0.000000000000000000, 1.000000000000000000 ) ) ;
#22132=ORIENTED_EDGE ( 'NONE', *, *, #13363, .F. ) ;
#22134=DIRECTION ( 'NONE',  ( -0.000000000000000000, -0.000000000000000000, -1.000000000000000000 ) ) ;
#22137=LINE ( 'NONE', #3692, #8669 ) ;
#22143=EDGE_CURVE ( 'NONE', #3047, #8203, #13892, .T. ) ;
#22158=CIRCLE ( 'NONE', #19828, 10.99999999999999645 ) ;
#22184=CIRCLE ( 'NONE', #21396, 1.500000000000001332 ) ;
#22187=DIRECTION ( 'NONE',  ( 0.000000000000000000, 0.000000000000000000, 1.000000000000000000 ) ) ;
#22189=CARTESIAN_POINT ( 'NONE',  ( 16.81886298599062002, 7.518780870797758809, 5.825851398835383499 ) ) ;
#22226=CARTESIAN_POINT ( 'NONE',  ( 0.000000000000000000, 45.00000000000000000, 27.00000000000000000 ) ) ;
#22246=EDGE_CURVE ( 'NONE', #5686, #12890, #15288, .T. ) ;
#22250=ORIENTED_EDGE ( 'NONE', *, *, #3479, .F. ) ;
#22252=LINE ( 'NONE', #20189, #5274 ) ;
#22275=AXIS2_PLACEMENT_3D ( 'NONE', #6693, #13643, #19764 ) ;
#22292=EDGE_LOOP ( 'NONE', ( #20388, #12221, #16277, #15917 ) ) ;
#22296=CARTESIAN_POINT ( 'NONE',  ( 15.57833309066360350, 5.219313726039665369, 7.987432870209364211 ) ) ;
#22300=ADVANCED_FACE ( 'NONE', ( #8475 ), #21307, .F. ) ;
#22311=VERTEX_POINT ( 'NONE', #2998 ) ;
#22315=CYLINDRICAL_SURFACE ( 'NONE', #15408, 11.00000000000000355 ) ;
#22329=CARTESIAN_POINT ( 'NONE',  ( -17.52854577772373190, 9.313395544511452684, -1.935253206038901608 ) ) ;
#22344=DIRECTION ( 'NONE',  ( 0.000000000000000000, 0.000000000000000000, 1.000000000000000000 ) ) ;
#22350=PLANE ( 'NONE',  #16478 ) ;
#22368=EDGE_LOOP ( 'NONE', ( #20774, #12198 ) ) ;
#22390=EDGE_CURVE ( 'NONE', #5827, #13474, #12369, .T. ) ;
#22396=ORIENTED_EDGE ( 'NONE', *, *, #21912, .T. ) ;
#22397=ORIENTED_EDGE ( 'NONE', *, *, #1949, .T. ) ;
#22404=ORIENTED_EDGE ( 'NONE', *, *, #3669, .F. ) ;
#22420=AXIS2_PLACEMENT_3D ( 'NONE', #10176, #941, #19373 ) ;
#22441=AXIS2_PLACEMENT_3D ( 'NONE', #15357, #490, #265 ) ;
#22444=CONICAL_SURFACE ( 'NONE', #2564, 1.999999999999994449, 1.029744258676653201 ) ;
#22451=ORIENTED_EDGE ( 'NONE', *, *, #149, .F. ) ;
#22455=CARTESIAN_POINT ( 'NONE',  ( -17.57797814737054054, 9.461914562436916754, -0.9781177603712974955 ) ) ;
#22459=ORIENTED_EDGE ( 'NONE', *, *, #13899, .F. ) ;
#22464=CYLINDRICAL_SURFACE ( 'NONE', #10683, 23.84999999999999432 ) ;
#22469=EDGE_CURVE ( 'NONE', #13972, #19865, #9059, .T. ) ;
#22471=DIRECTION ( 'NONE',  ( -1.000000000000000000, 0.000000000000000000, 0.000000000000000000 ) ) ;
#22480=ORIENTED_EDGE ( 'NONE', *, *, #8800, .T. ) ;
#22486=CARTESIAN_POINT ( 'NONE',  ( 14.91530227160598798, 1.623290104782669330, -9.365835742197232250 ) ) ;
#22496=FACE_OUTER_BOUND ( 'NONE', #7708, .T. ) ;
#22497=ORIENTED_EDGE ( 'NONE', *, *, #1917, .F. ) ;
#22501=EDGE_CURVE ( 'NONE', #23937, #6532, #22252, .T. ) ;
#22514=ORIENTED_EDGE ( 'NONE', *, *, #19579, .F. ) ;
#22550=DIRECTION ( 'NONE',  ( -0.000000000000000000, -0.000000000000000000, -1.000000000000000000 ) ) ;
#22568=EDGE_CURVE ( 'NONE', #5790, #15957, #20415, .T. ) ;
#22573=DIRECTION ( 'NONE',  ( -0.000000000000000000, -0.000000000000000000, -1.000000000000000000 ) ) ;
#22587=AXIS2_PLACEMENT_3D ( 'NONE', #19167, #15120, #17200 ) ;
#22594=ORIENTED_EDGE ( 'NONE', *, *, #16099, .T. ) ;
#22596=DIRECTION ( 'NONE',  ( 0.7071067811865660024, 0.000000000000000000, 0.7071067811865291430 ) ) ;
#22609=CARTESIAN_POINT ( 'NONE',  ( -18.50000000000000000, 15.23000000000000220, 27.00000000000000000 ) ) ;
#22610=ORIENTED_EDGE ( 'NONE', *, *, #346, .T. ) ;
#22613=VERTEX_POINT ( 'NONE', #17473 ) ;
#22615=ORIENTED_EDGE ( 'NONE', *, *, #24038, .F. ) ;
#22621=ORIENTED_EDGE ( 'NONE', *, *, #13088, .T. ) ;
#22624=CARTESIAN_POINT ( 'NONE',  ( 1.999999999999994449, 45.00000000000000000, -23.99999999999999645 ) ) ;
#22626=ADVANCED_FACE ( 'NONE', ( #5885 ), #22977, .F. ) ;
#22631=VERTEX_POINT ( 'NONE', #22866 ) ;
#22632=ORIENTED_EDGE ( 'NONE', *, *, #2766, .F. ) ;
#22640=FACE_OUTER_BOUND ( 'NONE', #4187, .T. ) ;
#22641=FACE_OUTER_BOUND ( 'NONE', #10419, .T. ) ;
#22642=AXIS2_PLACEMENT_3D ( 'NONE', #10206, #17669, #14725 ) ;
#22645=PLANE ( 'NONE',  #22725 ) ;
#22650=DIRECTION ( 'NONE',  ( -0.000000000000000000, -0.000000000000000000, -1.000000000000000000 ) ) ;
#22658=VECTOR ( 'NONE', #15296, 1000.000000000000000 ) ;
#22664=CARTESIAN_POINT ( 'NONE',  ( 23.90000000000000924, -29.50000000000000711, -27.00000000000000000 ) ) ;
#22685=( NAMED_UNIT ( * ) SI_UNIT ( $, .STERADIAN. ) SOLID_ANGLE_UNIT ( ) );
#22693=VECTOR ( 'NONE', #3180, 1000.000000000000000 ) ;
#22698=ADVANCED_FACE ( 'NONE', ( #17101 ), #13313, .F. ) ;
#22707=AXIS2_PLACEMENT_3D ( 'NONE', #19643, #2918, #8259 ) ;
#22725=AXIS2_PLACEMENT_3D ( 'NONE', #15173, #8589, #10537 ) ;
#22742=VERTEX_POINT ( 'NONE', #2604 ) ;
#22744=CARTESIAN_POINT ( 'NONE',  ( 41.99999999999999289, 6.781874047275040887E-15, 9.499999999999987566 ) ) ;
#22749=LINE ( 'NONE', #16874, #19244 ) ;
#22750=DIRECTION ( 'NONE',  ( -1.000000000000000000, 0.000000000000000000, 0.000000000000000000 ) ) ;
#22771=EDGE_CURVE ( 'NONE', #6272, #704, #19918, .T. ) ;
#22773=DIRECTION ( 'NONE',  ( 0.000000000000000000, 0.000000000000000000, 1.000000000000000000 ) ) ;
#22781=CARTESIAN_POINT ( 'NONE',  ( 15.07341617659254496, 4.495283618570412365, -8.379779594489210837 ) ) ;
#22792=CIRCLE ( 'NONE', #23960, 1.999999999999994449 ) ;
#22810=CARTESIAN_POINT ( 'NONE',  ( -1.999999999999994449, 45.00000000000000000, -23.99999999999999645 ) ) ;
#22812=CARTESIAN_POINT ( 'NONE',  ( -16.36153765883235423, 6.593687918952694460, -6.842832175870697142 ) ) ;
#22814=CARTESIAN_POINT ( 'NONE',  ( -41.99999999999999289, 0.000000000000000000, 10.50249999999999950 ) ) ;
#22834=ADVANCED_FACE ( 'NONE', ( #5044 ), #23592, .F. ) ;
#22849=LINE ( 'NONE', #13564, #1322 ) ;
#22851=EDGE_LOOP ( 'NONE', ( #19148, #23584, #16140, #6624 ) ) ;
#22854=EDGE_CURVE ( 'NONE', #13831, #11194, #2964, .T. ) ;
#22857=ORIENTED_EDGE ( 'NONE', *, *, #19604, .T. ) ;
#22862=VECTOR ( 'NONE', #3665, 1000.000000000000000 ) ;
#22864=EDGE_LOOP ( 'NONE', ( #2735, #10603, #4426, #20452 ) ) ;
#22866=CARTESIAN_POINT ( 'NONE',  ( 23.84999999999999432, -15.03999999999999559, 27.00000000000000000 ) ) ;
#22869=VERTEX_POINT ( 'NONE', #3322 ) ;
#22872=EDGE_LOOP ( 'NONE', ( #953, #22615, #55, #23183, #19824 ) ) ;
#22874=VERTEX_POINT ( 'NONE', #21865 ) ;
#22878=PRODUCT_DEFINITION_CONTEXT ( 'detailed design', #19315, 'design' ) ;
#22880=ORIENTED_EDGE ( 'NONE', *, *, #2001, .F. ) ;
#22885=VECTOR ( 'NONE', #184, 1000.000000000000000 ) ;
#22892=VERTEX_POINT ( 'NONE', #12457 ) ;
#22902=DIRECTION ( 'NONE',  ( -1.000000000000000000, 0.000000000000000000, 0.000000000000000000 ) ) ;
#22907=EDGE_CURVE ( 'NONE', #13474, #5422, #23462, .T. ) ;
#22913=EDGE_LOOP ( 'NONE', ( #20883, #17721, #5895, #2116 ) ) ;
#22929=CARTESIAN_POINT ( 'NONE',  ( 20.84999999999999432, -15.04000000000000448, 25.00000000000000000 ) ) ;
#22933=CARTESIAN_POINT ( 'NONE',  ( -16.19099482616364938, 6.271157271432195479, 7.149633965064785990 ) ) ;
#22934=CIRCLE ( 'NONE', #18641, 5.100000000000000533 ) ;
#22939=AXIS2_PLACEMENT_3D ( 'NONE', #8813, #8455, #16831 ) ;
#22944=ADVANCED_FACE ( 'NONE', ( #14655 ), #10855, .F. ) ;
#22954=ORIENTED_EDGE ( 'NONE', *, *, #9148, .T. ) ;
#22959=PLANE ( 'NONE',  #13575 ) ;
#22963=CARTESIAN_POINT ( 'NONE',  ( 30.44534269664589843, 40.40463133211081015, 27.00000000000000000 ) ) ;
#22965=ORIENTED_EDGE ( 'NONE', *, *, #19666, .T. ) ;
#22977=CYLINDRICAL_SURFACE ( 'NONE', #3718, 9.499999999999987566 ) ;
#22980=VECTOR ( 'NONE', #10663, 1000.000000000000000 ) ;
#22988=LINE ( 'NONE', #22744, #3987 ) ;
#22991=VERTEX_POINT ( 'NONE', #11659 ) ;
#23017=CARTESIAN_POINT ( 'NONE',  ( 0.000000000000000000, -15.23000000000000220, 27.00000000000000000 ) ) ;
#23021=CARTESIAN_POINT ( 'NONE',  ( -28.99999999999999645, -29.50000000000001066, 27.00000000000000000 ) ) ;
#23025=ORIENTED_EDGE ( 'NONE', *, *, #9581, .T. ) ;
#23028=ORIENTED_EDGE ( 'NONE', *, *, #13022, .F. ) ;
#23029=CARTESIAN_POINT ( 'NONE',  ( 0.000000000000000000, 45.00000000000000000, 27.00000000000000000 ) ) ;
#23046=CARTESIAN_POINT ( 'NONE',  ( -16.36913330654532217, 6.602951766536808265, 6.845624079409805773 ) ) ;
#23065=DIRECTION ( 'NONE',  ( -1.000000000000000000, 0.000000000000000000, 0.000000000000000000 ) ) ;
#23075=CARTESIAN_POINT ( 'NONE',  ( 20.85000000000000853, 15.03999999999999915, -25.00000000000000000 ) ) ;
#23078=VECTOR ( 'NONE', #11039, 1000.000000000000000 ) ;
#23088=DIRECTION ( 'NONE',  ( -0.000000000000000000, -0.000000000000000000, 1.000000000000000000 ) ) ;
#23089=EDGE_LOOP ( 'NONE', ( #8002, #20577, #17681, #23726 ) ) ;
#23091=VERTEX_POINT ( 'NONE', #17654 ) ;
#23097=VECTOR ( 'NONE', #7531, 1000.000000000000000 ) ;
#23100=AXIS2_PLACEMENT_3D ( 'NONE', #18897, #23384, #19470 ) ;
#23103=CIRCLE ( 'NONE', #12964, 1.500000000000001332 ) ;
#23119=AXIS2_PLACEMENT_3D ( 'NONE', #5640, #151, #4041 ) ;
#23129=ORIENTED_EDGE ( 'NONE', *, *, #14060, .T. ) ;
#23136=CARTESIAN_POINT ( 'NONE',  ( -17.49066032632880763, -9.200828712690862332, 2.414248458042551615 ) ) ;
#23141=ORIENTED_EDGE ( 'NONE', *, *, #4655, .F. ) ;
#23143=VECTOR ( 'NONE', #22106, 1000.000000000000000 ) ;
#23148=CARTESIAN_POINT ( 'NONE',  ( 17.06033556854817590, -8.068938288216797261, 5.036196554528626024 ) ) ;
#23150=AXIS2_PLACEMENT_3D ( 'NONE', #10282, #12355, #12093 ) ;
#23155=AXIS2_PLACEMENT_3D ( 'NONE', #347, #21071, #13257 ) ;
#23156=CARTESIAN_POINT ( 'NONE',  ( 41.99999999999999289, 6.904644888889564703E-15, 10.50249999999999950 ) ) ;
#23173=AXIS2_PLACEMENT_3D ( 'NONE', #19397, #11930, #10210 ) ;
#23175=DIRECTION ( 'NONE',  ( -0.000000000000000000, -0.000000000000000000, -1.000000000000000000 ) ) ;
#23176=LINE ( 'NONE', #9718, #2435 ) ;
#23183=ORIENTED_EDGE ( 'NONE', *, *, #15201, .T. ) ;
#23206=FACE_OUTER_BOUND ( 'NONE', #20347, .T. ) ;
#23207=CARTESIAN_POINT ( 'NONE',  ( 34.10000000000000853, 29.50000000000000000, 27.00000000000000000 ) ) ;
#23215=ORIENTED_EDGE ( 'NONE', *, *, #1640, .T. ) ;
#23219=CARTESIAN_POINT ( 'NONE',  ( 0.000000000000000000, -15.03999999999999915, -27.00000000000000000 ) ) ;
#23223=CARTESIAN_POINT ( 'NONE',  ( -14.51962751333974033, -3.765689428759031010, -8.721787840009202597 ) ) ;
#23226=ADVANCED_FACE ( 'NONE', ( #17797 ), #8384, .T. ) ;
#23232=DIRECTION ( 'NONE',  ( -0.000000000000000000, -0.000000000000000000, -1.000000000000000000 ) ) ;
#23247=ADVANCED_FACE ( 'NONE', ( #19260 ), #2542, .F. ) ;
#23270=CYLINDRICAL_SURFACE ( 'NONE', #2501, 1.999999999999994449 ) ;
#23278=DIRECTION ( 'NONE',  ( 0.000000000000000000, 0.000000000000000000, 1.000000000000000000 ) ) ;
#23279=LINE ( 'NONE', #19847, #15223 ) ;
#23281=CARTESIAN_POINT ( 'NONE',  ( 15.00000000000000355, 0.3238088414458227260, 9.499999999999989342 ) ) ;
#23285=EDGE_LOOP ( 'NONE', ( #24052, #10834, #17014, #7946, #15055 ) ) ;
#23306=ORIENTED_EDGE ( 'NONE', *, *, #17244, .T. ) ;
#23309=DIRECTION ( 'NONE',  ( 4.613626265895764052E-16, -1.000000000000000000, 0.000000000000000000 ) ) ;
#23324=DIRECTION ( 'NONE',  ( -0.000000000000000000, 1.000000000000000000, -0.000000000000000000 ) ) ;
#23330=EDGE_LOOP ( 'NONE', ( #4555, #16310 ) ) ;
#23345=VERTEX_POINT ( 'NONE', #12405 ) ;
#23349=CARTESIAN_POINT ( 'NONE',  ( -40.99749999999999517, 0.000000000000000000, 9.499999999999994671 ) ) ;
#23351=DIRECTION ( 'NONE',  ( -0.000000000000000000, 1.000000000000000000, -0.000000000000000000 ) ) ;
#23352=VERTEX_POINT ( 'NONE', #5337 ) ;
#23362=EDGE_CURVE ( 'NONE', #10814, #9670, #8614, .T. ) ;
#23384=DIRECTION ( 'NONE',  ( 0.4011779117250717785, 0.9160001545545232160, -0.000000000000000000 ) ) ;
#23392=DIRECTION ( 'NONE',  ( -0.000000000000000000, -1.000000000000000000, -0.000000000000000000 ) ) ;
#23398=CIRCLE ( 'NONE', #21451, 10.50249999999999950 ) ;
#23403=VERTEX_POINT ( 'NONE', #19757 ) ;
#23407=VERTEX_POINT ( 'NONE', #23997 ) ;
#23432=FACE_OUTER_BOUND ( 'NONE', #2528, .T. ) ;
#23437=DIRECTION ( 'NONE',  ( 0.9160001545545232160, -0.4011779117250717785, -0.000000000000000000 ) ) ;
#23444=ORIENTED_EDGE ( 'NONE', *, *, #21474, .T. ) ;
#23457=CARTESIAN_POINT ( 'NONE',  ( -20.85000000000000853, 15.04000000000000092, 25.00000000000000000 ) ) ;
#23460=VERTEX_POINT ( 'NONE', #7618 ) ;
#23462=LINE ( 'NONE', #8554, #23627 ) ;
#23464=VERTEX_POINT ( 'NONE', #14819 ) ;
#23467=ORIENTED_EDGE ( 'NONE', *, *, #22125, .T. ) ;
#23468=VECTOR ( 'NONE', #23175, 1000.000000000000000 ) ;
#23470=AXIS2_PLACEMENT_3D ( 'NONE', #2693, #8156, #23065 ) ;
#23471=ORIENTED_EDGE ( 'NONE', *, *, #1753, .F. ) ;
#23489=AXIS2_PLACEMENT_3D ( 'NONE', #20647, #6007, #9754 ) ;
#23495=CARTESIAN_POINT ( 'NONE',  ( 40.00000000000000711, 29.50000000000000000, 27.00000000000000000 ) ) ;
#23497=CARTESIAN_POINT ( 'NONE',  ( -17.32314925601269806, -8.733074366907757735, -3.769949228126193486 ) ) ;
#23499=DIRECTION ( 'NONE',  ( 1.000000000000000000, -4.613626265895763066E-16, 0.000000000000000000 ) ) ;
#23505=CARTESIAN_POINT ( 'NONE',  ( 17.52854577772373190, -9.313395544511447355, -1.935253206038896279 ) ) ;
#23522=ADVANCED_FACE ( 'NONE', ( #4106 ), #17013, .F. ) ;
#23523=CARTESIAN_POINT ( 'NONE',  ( -41.49999999999999289, 27.79189783386526358, 27.00000000000000000 ) ) ;
#23529=CYLINDRICAL_SURFACE ( 'NONE', #7583, 5.100000000000000533 ) ;
#23553=VECTOR ( 'NONE', #16265, 1000.000000000000000 ) ;
#23565=VERTEX_POINT ( 'NONE', #2749 ) ;
#23574=ADVANCED_FACE ( 'NONE', ( #13494 ), #4939, .F. ) ;
#23584=ORIENTED_EDGE ( 'NONE', *, *, #11836, .F. ) ;
#23587=DIRECTION ( 'NONE',  ( 1.000000000000000000, 0.000000000000000000, 0.000000000000000000 ) ) ;
#23592=CYLINDRICAL_SURFACE ( 'NONE', #5294, 1.500000000000001332 ) ;
#23602=ORIENTED_EDGE ( 'NONE', *, *, #21191, .T. ) ;
#23605=DIRECTION ( 'NONE',  ( -1.000000000000000000, 0.000000000000000000, 0.000000000000000000 ) ) ;
#23627=VECTOR ( 'NONE', #1387, 1000.000000000000000 ) ;
#23629=ORIENTED_EDGE ( 'NONE', *, *, #19883, .T. ) ;
#23635=DIRECTION ( 'NONE',  ( -0.000000000000000000, -0.000000000000000000, -1.000000000000000000 ) ) ;
#23639=CARTESIAN_POINT ( 'NONE',  ( 16.44572538483723179, -6.755397553796130161, -6.683320200552548052 ) ) ;
#23641=EDGE_CURVE ( 'NONE', #9464, #5416, #21174, .T. ) ;
#23650=ORIENTED_EDGE ( 'NONE', *, *, #17495, .F. ) ;
#23654=DIRECTION ( 'NONE',  ( 0.000000000000000000, 0.000000000000000000, 1.000000000000000000 ) ) ;
#23666=EDGE_CURVE ( 'NONE', #7845, #886, #13111, .T. ) ;
#23680=CARTESIAN_POINT ( 'NONE',  ( 39.99999999999999289, 29.50000000000000000, 27.00000000000000000 ) ) ;
#23701=DIRECTION ( 'NONE',  ( -0.000000000000000000, -0.000000000000000000, -1.000000000000000000 ) ) ;
#23715=PLANE ( 'NONE',  #3821 ) ;
#23716=ORIENTED_EDGE ( 'NONE', *, *, #12876, .T. ) ;
#23723=CARTESIAN_POINT ( 'NONE',  ( 1.999999999999994449, -45.00000000000000000, -26.97499999999999432 ) ) ;
#23726=ORIENTED_EDGE ( 'NONE', *, *, #21007, .T. ) ;
#23745=DIRECTION ( 'NONE',  ( 1.000000000000000000, 0.000000000000000000, 0.000000000000000000 ) ) ;
#23761=DIRECTION ( 'NONE',  ( -1.000000000000000000, 0.000000000000000000, 0.000000000000000000 ) ) ;
#23771=CARTESIAN_POINT ( 'NONE',  ( 0.000000000000000000, -15.03999999999999915, 25.00000000000000000 ) ) ;
#23800=CARTESIAN_POINT ( 'NONE',  ( -14.91530227160598265, 1.623290104782663335, 9.365835742197235803 ) ) ;
#23804=CARTESIAN_POINT ( 'NONE',  ( -41.49999999999999289, -27.79189783386527779, 27.00000000000000000 ) ) ;
#23818=DIRECTION ( 'NONE',  ( -1.000000000000000000, 0.000000000000000000, 0.000000000000000000 ) ) ;
#23827=LINE ( 'NONE', #14418, #11773 ) ;
#23829=CONICAL_SURFACE ( 'NONE', #13272, 1.999999999999994449, 1.029744258676653201 ) ;
#23830=CARTESIAN_POINT ( 'NONE',  ( 14.51962751333974389, 3.765689428759029234, 27.00000000000000000 ) ) ;
#23835=ADVANCED_FACE ( 'NONE', ( #21497 ), #2466, .F. ) ;
#23840=DIRECTION ( 'NONE',  ( -0.000000000000000000, -0.000000000000000000, -1.000000000000000000 ) ) ;
#23842=ORIENTED_EDGE ( 'NONE', *, *, #19958, .F. ) ;
#23851=CARTESIAN_POINT ( 'NONE',  ( -14.79227890392045275, 2.568991289487078333, -9.169086800441911933 ) ) ;
#23892=DIRECTION ( 'NONE',  ( -1.000000000000000000, 0.000000000000000000, 0.000000000000000000 ) ) ;
#23907=AXIS2_PLACEMENT_3D ( 'NONE', #5420, #7594, #416 ) ;
#23919=DIRECTION ( 'NONE',  ( -1.000000000000000000, -0.000000000000000000, -0.000000000000000000 ) ) ;
#23921=DIRECTION ( 'NONE',  ( 0.000000000000000000, 0.000000000000000000, 1.000000000000000000 ) ) ;
#23926=AXIS2_PLACEMENT_3D ( 'NONE', #14199, #7550, #10530 ) ;
#23930=AXIS2_PLACEMENT_3D ( 'NONE', #19242, #700, #15554 ) ;
#23933=ORIENTED_EDGE ( 'NONE', *, *, #13931, .F. ) ;
#23937=VERTEX_POINT ( 'NONE', #8307 ) ;
#23940=AXIS2_PLACEMENT_3D ( 'NONE', #1806, #18037, #7393 ) ;
#23944=CYLINDRICAL_SURFACE ( 'NONE', #18489, 4.999999999999997335 ) ;
#23950=ORIENTED_EDGE ( 'NONE', *, *, #3888, .T. ) ;
#23959=CYLINDRICAL_SURFACE ( 'NONE', #5512, 50.00000000000000000 ) ;
#23960=AXIS2_PLACEMENT_3D ( 'NONE', #222, #7501, #7631 ) ;
#23963=CONICAL_SURFACE ( 'NONE', #5641, 1.999999999999994449, 1.029744258676653201 ) ;
#23997=CARTESIAN_POINT ( 'NONE',  ( 18.50000000000000000, 15.23000000000000398, 27.00000000000000000 ) ) ;
#24008=LINE ( 'NONE', #11042, #7095 ) ;
#24009=EDGE_CURVE ( 'NONE', #704, #18466, #7651, .T. ) ;
#24013=ADVANCED_FACE ( 'NONE', ( #3435, #14517, #16597, #16245, #7205, #24046, #3316, #14168 ), #22119, .F. ) ;
#24038=EDGE_CURVE ( 'NONE', #19120, #13598, #14289, .T. ) ;
#24046=FACE_BOUND ( 'NONE', #15796, .T. ) ;
#24050=CARTESIAN_POINT ( 'NONE',  ( -14.51962751333974033, -3.765689428759031010, 8.721787840009202597 ) ) ;
#24052=ORIENTED_EDGE ( 'NONE', *, *, #2179, .F. ) ;
#24058=VERTEX_POINT ( 'NONE', #7077 ) ;
#24061=CARTESIAN_POINT ( 'NONE',  ( -1.999999999999994449, -45.00000000000000000, 23.99999999999999645 ) ) ;
#24063=CARTESIAN_POINT ( 'NONE',  ( 0.000000000000000000, -45.00000000000000000, -27.00000000000000000 ) ) ;
#24076=EDGE_LOOP ( 'NONE', ( #18833, #746, #9091, #23650 ) ) ;
#24085=CIRCLE ( 'NONE', #16688, 1.999999999999994449 ) ;
#24128=COLOUR_RGB('Dark Blue',0.08,0.2,0.34);
#24129=FILL_AREA_STYLE_COLOUR('',#24128);
#24130=FILL_AREA_STYLE('',(#24129));
#24131=SURFACE_STYLE_FILL_AREA(#24130);
#24132=SURFACE_SIDE_STYLE('',(#24131));
#24133=SURFACE_STYLE_USAGE(.BOTH.,#24132);
#24134=PRESENTATION_STYLE_ASSIGNMENT((#24133));
ENDSEC;
END-ISO-10303-21;
